ISO-10303-21;
HEADER;
/* Generated by software containing ST-Developer
 * from STEP Tools, Inc. (www.steptools.com) 
 */

FILE_DESCRIPTION(
/* description */ ('STEP AP214'),
/* implementation_level */ '2;1');

FILE_NAME(
/* name */ 'Zinc-Plated Steel Hex Nut.step',
/* time_stamp */ '2026-11-14T06:34:07-08:00',
/* author */ (''),
/* organization */ (''),
/* preprocessor_version */ 'ST-DEVELOPER v20.2',
/* originating_system */ 'Autodesk Translation Framework v15.17.0.0',
/* authorisation */ '');

FILE_SCHEMA (('AUTOMOTIVE_DESIGN { 1 0 10303 214 3 1 1 }'));
ENDSEC;

DATA;
#10=MECHANICAL_DESIGN_GEOMETRIC_PRESENTATION_REPRESENTATION('',(#7323),#310623);
#1738=(
BOUNDED_CURVE()
B_SPLINE_CURVE(2,(#309301,#309302,#309303,#309304,#309305,#309306,#309307,
#309308,#309309,#309310,#309311,#309312,#309313),.UNSPECIFIED.,.F.,.F.)
B_SPLINE_CURVE_WITH_KNOTS((3,2,2,2,2,2,3),(0.670198248522263,0.685091542933869,
0.699984837345475,0.714878131757081,0.729771426168687,0.744664720580293,
0.750623093706636),.UNSPECIFIED.)
CURVE()
GEOMETRIC_REPRESENTATION_ITEM()
RATIONAL_B_SPLINE_CURVE((1.,0.951056516295154,1.,0.951056516295154,1.,0.951056516295154,
1.,0.951056516295154,1.,0.951056516295154,1.,0.980419138307685,0.976505741029048))
REPRESENTATION_ITEM('')
);
#1739=(
BOUNDED_CURVE()
B_SPLINE_CURVE(2,(#309314,#309315,#309316,#309317,#309318,#309319,#309320,
#309321,#309322,#309323,#309324,#309325,#309326,#309327,#309328),
 .UNSPECIFIED.,.F.,.F.)
B_SPLINE_CURVE_WITH_KNOTS((3,2,2,2,2,2,2,3),(0.642857142857143,0.657142857142857,
0.671428571428571,0.685714285714286,0.7,0.714285714285714,0.728571428571428,
0.737776488038992),.UNSPECIFIED.)
CURVE()
GEOMETRIC_REPRESENTATION_ITEM()
RATIONAL_B_SPLINE_CURVE((1.,0.951056516295154,1.,0.951056516295154,1.,0.951056516295154,
1.,0.951056516295154,1.,0.951056516295154,1.,0.951056516295154,1.,0.968463062536303,
0.977568038941547))
REPRESENTATION_ITEM('')
);
#1740=(
BOUNDED_CURVE()
B_SPLINE_CURVE(2,(#309333,#309334,#309335,#309336,#309337,#309338,#309339,
#309340,#309341,#309342,#309343,#309344,#309345,#309346,#309347,#309348,
#309349,#309350,#309351,#309352,#309353),.UNSPECIFIED.,.F.,.F.)
B_SPLINE_CURVE_WITH_KNOTS((3,2,2,2,2,2,2,2,2,2,3),(0.521265304406204,0.53615859881781,
0.551051893229416,0.565945187641022,0.580838482052628,0.595731776464233,
0.610625070875839,0.625518365287445,0.640411659699051,0.655304954110657,
0.670198248522263),.UNSPECIFIED.)
CURVE()
GEOMETRIC_REPRESENTATION_ITEM()
RATIONAL_B_SPLINE_CURVE((1.,0.951056516295154,1.,0.951056516295154,1.,0.951056516295154,
1.,0.951056516295154,1.,0.951056516295154,1.,0.951056516295154,1.,0.951056516295154,
1.,0.951056516295154,1.,0.951056516295154,1.,0.951056516295154,1.))
REPRESENTATION_ITEM('')
);
#1741=(
BOUNDED_CURVE()
B_SPLINE_CURVE(2,(#309354,#309355,#309356,#309357,#309358,#309359,#309360,
#309361,#309362,#309363,#309364,#309365,#309366,#309367,#309368,#309369,
#309370,#309371,#309372,#309373,#309374),.UNSPECIFIED.,.F.,.F.)
B_SPLINE_CURVE_WITH_KNOTS((3,2,2,2,2,2,2,2,2,2,3),(0.5,0.514285714285714,
0.528571428571429,0.542857142857143,0.557142857142857,0.571428571428571,
0.585714285714286,0.6,0.614285714285714,0.628571428571429,0.642857142857143),
 .UNSPECIFIED.)
CURVE()
GEOMETRIC_REPRESENTATION_ITEM()
RATIONAL_B_SPLINE_CURVE((1.,0.951056516295154,1.,0.951056516295154,1.,0.951056516295154,
1.,0.951056516295154,1.,0.951056516295154,1.,0.951056516295154,1.,0.951056516295154,
1.,0.951056516295154,1.,0.951056516295154,1.,0.951056516295154,1.))
REPRESENTATION_ITEM('')
);
#1742=(
BOUNDED_CURVE()
B_SPLINE_CURVE(2,(#309379,#309380,#309381,#309382,#309383,#309384,#309385,
#309386,#309387,#309388,#309389,#309390,#309391,#309392,#309393,#309394,
#309395,#309396,#309397,#309398,#309399),.UNSPECIFIED.,.F.,.F.)
B_SPLINE_CURVE_WITH_KNOTS((3,2,2,2,2,2,2,2,2,2,3),(0.372332360290144,0.38722565470175,
0.402118949113356,0.417012243524962,0.431905537936568,0.446798832348174,
0.46169212675978,0.476585421171386,0.491478715582992,0.506372009994598,
0.521265304406204),.UNSPECIFIED.)
CURVE()
GEOMETRIC_REPRESENTATION_ITEM()
RATIONAL_B_SPLINE_CURVE((1.,0.951056516295154,1.,0.951056516295154,1.,0.951056516295154,
1.,0.951056516295154,1.,0.951056516295154,1.,0.951056516295154,1.,0.951056516295154,
1.,0.951056516295154,1.,0.951056516295154,1.,0.951056516295154,1.))
REPRESENTATION_ITEM('')
);
#1743=(
BOUNDED_CURVE()
B_SPLINE_CURVE(2,(#309400,#309401,#309402,#309403,#309404,#309405,#309406,
#309407,#309408,#309409,#309410,#309411,#309412,#309413,#309414,#309415,
#309416,#309417,#309418,#309419,#309420),.UNSPECIFIED.,.F.,.F.)
B_SPLINE_CURVE_WITH_KNOTS((3,2,2,2,2,2,2,2,2,2,3),(0.357142857142857,0.371428571428571,
0.385714285714286,0.4,0.414285714285715,0.428571428571428,0.442857142857143,
0.457142857142857,0.471428571428571,0.485714285714286,0.5),
 .UNSPECIFIED.)
CURVE()
GEOMETRIC_REPRESENTATION_ITEM()
RATIONAL_B_SPLINE_CURVE((1.,0.951056516295154,1.,0.951056516295154,1.,0.951056516295154,
1.,0.951056516295154,1.,0.951056516295154,1.,0.951056516295154,1.,0.951056516295154,
1.,0.951056516295154,1.,0.951056516295154,1.,0.951056516295154,1.))
REPRESENTATION_ITEM('')
);
#1744=(
BOUNDED_CURVE()
B_SPLINE_CURVE(2,(#309427,#309428,#309429),.UNSPECIFIED.,.F.,.F.)
B_SPLINE_CURVE_WITH_KNOTS((3,3),(0.212227443337166,0.223399416174085),
 .UNSPECIFIED.)
CURVE()
GEOMETRIC_REPRESENTATION_ITEM()
RATIONAL_B_SPLINE_CURVE((0.981652774597814,0.963285808003053,1.))
REPRESENTATION_ITEM('')
);
#1745=(
BOUNDED_CURVE()
B_SPLINE_CURVE(2,(#309746,#309747,#309748,#309749,#309750,#309751,#309752,
#309753,#309754,#309755,#309756,#309757,#309758,#309759,#309760,#309761,
#309762,#309763,#309764,#309765,#309766),.UNSPECIFIED.,.F.,.F.)
B_SPLINE_CURVE_WITH_KNOTS((3,2,2,2,2,2,2,2,2,2,3),(0.223399416174085,0.23829271058569,
0.253186004997297,0.268079299408903,0.282972593820508,0.297865888232115,
0.312759182643721,0.327652477055327,0.342545771466932,0.357439065878539,
0.372332360290144),.UNSPECIFIED.)
CURVE()
GEOMETRIC_REPRESENTATION_ITEM()
RATIONAL_B_SPLINE_CURVE((1.,0.951056516295154,1.,0.951056516295154,1.,0.951056516295154,
1.,0.951056516295154,1.,0.951056516295154,1.,0.951056516295154,1.,0.951056516295154,
1.,0.951056516295154,1.,0.951056516295154,1.,0.951056516295154,1.))
REPRESENTATION_ITEM('')
);
#1746=(
BOUNDED_CURVE()
B_SPLINE_CURVE(2,(#309820,#309821,#309822,#309823,#309824,#309825,#309826,
#309827,#309828,#309829,#309830,#309831,#309832,#309833,#309834,#309835,
#309836,#309837,#309838,#309839,#309840),.UNSPECIFIED.,.F.,.F.)
B_SPLINE_CURVE_WITH_KNOTS((3,2,2,2,2,2,2,2,2,2,3),(0.221361545916683,0.228571428571428,
0.242857142857143,0.257142857142857,0.271428571428572,0.285714285714286,
0.3,0.314285714285715,0.328571428571429,0.342857142857143,0.357142857142857),
 .UNSPECIFIED.)
CURVE()
GEOMETRIC_REPRESENTATION_ITEM()
RATIONAL_B_SPLINE_CURVE((0.975530412919128,0.97529862580415,1.,0.951056516295154,
1.,0.951056516295154,1.,0.951056516295154,1.,0.951056516295154,1.,0.951056516295154,
1.,0.951056516295154,1.,0.951056516295154,1.,0.951056516295154,1.,0.951056516295154,
1.))
REPRESENTATION_ITEM('')
);
#1747=(
BOUNDED_CURVE()
B_SPLINE_CURVE(2,(#310374,#310375,#310376),.UNSPECIFIED.,.F.,.F.)
B_SPLINE_CURVE_WITH_KNOTS((3,3),(1.8359668034886,2.908605540086),
 .UNSPECIFIED.)
CURVE()
GEOMETRIC_REPRESENTATION_ITEM()
RATIONAL_B_SPLINE_CURVE((1.8663905512715,2.00276625701356,2.00276625701356))
REPRESENTATION_ITEM('')
);
#1748=(
BOUNDED_CURVE()
B_SPLINE_CURVE(2,(#310378,#310379,#310380),.UNSPECIFIED.,.F.,.F.)
B_SPLINE_CURVE_WITH_KNOTS((3,3),(2.908605540086,3.98124427668513),
 .UNSPECIFIED.)
CURVE()
GEOMETRIC_REPRESENTATION_ITEM()
RATIONAL_B_SPLINE_CURVE((2.00276625701356,2.00276625701356,1.86639055127106))
REPRESENTATION_ITEM('')
);
#1749=(
BOUNDED_CURVE()
B_SPLINE_CURVE(2,(#310383,#310384,#310385),.UNSPECIFIED.,.F.,.F.)
B_SPLINE_CURVE_WITH_KNOTS((3,3),(1.83596680348874,2.908605540086),
 .UNSPECIFIED.)
CURVE()
GEOMETRIC_REPRESENTATION_ITEM()
RATIONAL_B_SPLINE_CURVE((1.86639055127154,2.00276625701356,2.00276625701356))
REPRESENTATION_ITEM('')
);
#1750=(
BOUNDED_CURVE()
B_SPLINE_CURVE(2,(#310387,#310388,#310389),.UNSPECIFIED.,.F.,.F.)
B_SPLINE_CURVE_WITH_KNOTS((3,3),(2.908605540086,3.98124427668513),
 .UNSPECIFIED.)
CURVE()
GEOMETRIC_REPRESENTATION_ITEM()
RATIONAL_B_SPLINE_CURVE((2.00276625701356,2.00276625701356,1.86639055127106))
REPRESENTATION_ITEM('')
);
#1751=(
BOUNDED_CURVE()
B_SPLINE_CURVE(2,(#310392,#310393,#310394),.UNSPECIFIED.,.F.,.F.)
B_SPLINE_CURVE_WITH_KNOTS((3,3),(1.83596680348874,2.908605540086),
 .UNSPECIFIED.)
CURVE()
GEOMETRIC_REPRESENTATION_ITEM()
RATIONAL_B_SPLINE_CURVE((1.86639055127154,2.00276625701356,2.00276625701356))
REPRESENTATION_ITEM('')
);
#1752=(
BOUNDED_CURVE()
B_SPLINE_CURVE(2,(#310396,#310397,#310398),.UNSPECIFIED.,.F.,.F.)
B_SPLINE_CURVE_WITH_KNOTS((3,3),(2.908605540086,3.9812442766844),
 .UNSPECIFIED.)
CURVE()
GEOMETRIC_REPRESENTATION_ITEM()
RATIONAL_B_SPLINE_CURVE((2.00276625701356,2.00276625701356,1.86639055127125))
REPRESENTATION_ITEM('')
);
#1753=(
BOUNDED_CURVE()
B_SPLINE_CURVE(2,(#310401,#310402,#310403),.UNSPECIFIED.,.F.,.F.)
B_SPLINE_CURVE_WITH_KNOTS((3,3),(1.8359668034886,2.908605540086),
 .UNSPECIFIED.)
CURVE()
GEOMETRIC_REPRESENTATION_ITEM()
RATIONAL_B_SPLINE_CURVE((1.8663905512715,2.00276625701356,2.00276625701356))
REPRESENTATION_ITEM('')
);
#1754=(
BOUNDED_CURVE()
B_SPLINE_CURVE(2,(#310405,#310406,#310407),.UNSPECIFIED.,.F.,.F.)
B_SPLINE_CURVE_WITH_KNOTS((3,3),(2.908605540086,3.98124427668513),
 .UNSPECIFIED.)
CURVE()
GEOMETRIC_REPRESENTATION_ITEM()
RATIONAL_B_SPLINE_CURVE((2.00276625701356,2.00276625701356,1.86639055127106))
REPRESENTATION_ITEM('')
);
#1755=(
BOUNDED_CURVE()
B_SPLINE_CURVE(2,(#310410,#310411,#310412),.UNSPECIFIED.,.F.,.F.)
B_SPLINE_CURVE_WITH_KNOTS((3,3),(1.83596680348875,2.908605540086),
 .UNSPECIFIED.)
CURVE()
GEOMETRIC_REPRESENTATION_ITEM()
RATIONAL_B_SPLINE_CURVE((1.86639055127154,2.00276625701356,2.00276625701356))
REPRESENTATION_ITEM('')
);
#1756=(
BOUNDED_CURVE()
B_SPLINE_CURVE(2,(#310414,#310415,#310416),.UNSPECIFIED.,.F.,.F.)
B_SPLINE_CURVE_WITH_KNOTS((3,3),(2.908605540086,3.98124427668513),
 .UNSPECIFIED.)
CURVE()
GEOMETRIC_REPRESENTATION_ITEM()
RATIONAL_B_SPLINE_CURVE((2.00276625701356,2.00276625701356,1.86639055127106))
REPRESENTATION_ITEM('')
);
#1757=(
BOUNDED_CURVE()
B_SPLINE_CURVE(2,(#310419,#310420,#310421),.UNSPECIFIED.,.F.,.F.)
B_SPLINE_CURVE_WITH_KNOTS((3,3),(1.83596680348874,2.908605540086),
 .UNSPECIFIED.)
CURVE()
GEOMETRIC_REPRESENTATION_ITEM()
RATIONAL_B_SPLINE_CURVE((1.86639055127154,2.00276625701356,2.00276625701356))
REPRESENTATION_ITEM('')
);
#1758=(
BOUNDED_CURVE()
B_SPLINE_CURVE(2,(#310422,#310423,#310424),.UNSPECIFIED.,.F.,.F.)
B_SPLINE_CURVE_WITH_KNOTS((3,3),(2.908605540086,3.9812442766844),
 .UNSPECIFIED.)
CURVE()
GEOMETRIC_REPRESENTATION_ITEM()
RATIONAL_B_SPLINE_CURVE((2.00276625701356,2.00276625701356,1.86639055127125))
REPRESENTATION_ITEM('')
);
#1759=(
BOUNDED_CURVE()
B_SPLINE_CURVE(2,(#310428,#310429,#310430),.UNSPECIFIED.,.F.,.F.)
B_SPLINE_CURVE_WITH_KNOTS((3,3),(-2.908605540086,-1.83596680348895),
 .UNSPECIFIED.)
CURVE()
GEOMETRIC_REPRESENTATION_ITEM()
RATIONAL_B_SPLINE_CURVE((2.00276625701356,2.00276625701356,1.86639055127159))
REPRESENTATION_ITEM('')
);
#1760=(
BOUNDED_CURVE()
B_SPLINE_CURVE(2,(#310432,#310433,#310434),.UNSPECIFIED.,.F.,.F.)
B_SPLINE_CURVE_WITH_KNOTS((3,3),(-3.98124427668322,-2.90860554008599),
 .UNSPECIFIED.)
CURVE()
GEOMETRIC_REPRESENTATION_ITEM()
RATIONAL_B_SPLINE_CURVE((1.86639055127155,2.00276625701356,2.00276625701356))
REPRESENTATION_ITEM('')
);
#1761=(
BOUNDED_CURVE()
B_SPLINE_CURVE(2,(#310437,#310438,#310439),.UNSPECIFIED.,.F.,.F.)
B_SPLINE_CURVE_WITH_KNOTS((3,3),(-2.90860554008599,-1.83596680348895),
 .UNSPECIFIED.)
CURVE()
GEOMETRIC_REPRESENTATION_ITEM()
RATIONAL_B_SPLINE_CURVE((2.00276625701356,2.00276625701356,1.86639055127159))
REPRESENTATION_ITEM('')
);
#1762=(
BOUNDED_CURVE()
B_SPLINE_CURVE(2,(#310441,#310442,#310443),.UNSPECIFIED.,.F.,.F.)
B_SPLINE_CURVE_WITH_KNOTS((3,3),(-3.98124427668324,-2.908605540086),
 .UNSPECIFIED.)
CURVE()
GEOMETRIC_REPRESENTATION_ITEM()
RATIONAL_B_SPLINE_CURVE((1.86639055127154,2.00276625701356,2.00276625701356))
REPRESENTATION_ITEM('')
);
#1763=(
BOUNDED_CURVE()
B_SPLINE_CURVE(2,(#310446,#310447,#310448),.UNSPECIFIED.,.F.,.F.)
B_SPLINE_CURVE_WITH_KNOTS((3,3),(-2.908605540086,-1.83596680348886),
 .UNSPECIFIED.)
CURVE()
GEOMETRIC_REPRESENTATION_ITEM()
RATIONAL_B_SPLINE_CURVE((2.00276625701356,2.00276625701356,1.86639055127157))
REPRESENTATION_ITEM('')
);
#1764=(
BOUNDED_CURVE()
B_SPLINE_CURVE(2,(#310450,#310451,#310452),.UNSPECIFIED.,.F.,.F.)
B_SPLINE_CURVE_WITH_KNOTS((3,3),(-3.98124427668322,-2.908605540086),
 .UNSPECIFIED.)
CURVE()
GEOMETRIC_REPRESENTATION_ITEM()
RATIONAL_B_SPLINE_CURVE((1.86639055127154,2.00276625701356,2.00276625701356))
REPRESENTATION_ITEM('')
);
#1765=(
BOUNDED_CURVE()
B_SPLINE_CURVE(2,(#310455,#310456,#310457),.UNSPECIFIED.,.F.,.F.)
B_SPLINE_CURVE_WITH_KNOTS((3,3),(-2.908605540086,-1.83596680348895),
 .UNSPECIFIED.)
CURVE()
GEOMETRIC_REPRESENTATION_ITEM()
RATIONAL_B_SPLINE_CURVE((2.00276625701356,2.00276625701356,1.86639055127159))
REPRESENTATION_ITEM('')
);
#1766=(
BOUNDED_CURVE()
B_SPLINE_CURVE(2,(#310459,#310460,#310461),.UNSPECIFIED.,.F.,.F.)
B_SPLINE_CURVE_WITH_KNOTS((3,3),(-3.98124427668322,-2.908605540086),
 .UNSPECIFIED.)
CURVE()
GEOMETRIC_REPRESENTATION_ITEM()
RATIONAL_B_SPLINE_CURVE((1.86639055127154,2.00276625701356,2.00276625701356))
REPRESENTATION_ITEM('')
);
#1767=(
BOUNDED_CURVE()
B_SPLINE_CURVE(2,(#310464,#310465,#310466),.UNSPECIFIED.,.F.,.F.)
B_SPLINE_CURVE_WITH_KNOTS((3,3),(-2.908605540086,-1.83596680348895),
 .UNSPECIFIED.)
CURVE()
GEOMETRIC_REPRESENTATION_ITEM()
RATIONAL_B_SPLINE_CURVE((2.00276625701356,2.00276625701356,1.86639055127159))
REPRESENTATION_ITEM('')
);
#1768=(
BOUNDED_CURVE()
B_SPLINE_CURVE(2,(#310468,#310469,#310470),.UNSPECIFIED.,.F.,.F.)
B_SPLINE_CURVE_WITH_KNOTS((3,3),(-3.98124427668324,-2.908605540086),
 .UNSPECIFIED.)
CURVE()
GEOMETRIC_REPRESENTATION_ITEM()
RATIONAL_B_SPLINE_CURVE((1.86639055127154,2.00276625701356,2.00276625701356))
REPRESENTATION_ITEM('')
);
#1769=(
BOUNDED_CURVE()
B_SPLINE_CURVE(2,(#310473,#310474,#310475),.UNSPECIFIED.,.F.,.F.)
B_SPLINE_CURVE_WITH_KNOTS((3,3),(-2.908605540086,-1.83596680348886),
 .UNSPECIFIED.)
CURVE()
GEOMETRIC_REPRESENTATION_ITEM()
RATIONAL_B_SPLINE_CURVE((2.00276625701356,2.00276625701356,1.86639055127157))
REPRESENTATION_ITEM('')
);
#1770=(
BOUNDED_CURVE()
B_SPLINE_CURVE(2,(#310476,#310477,#310478),.UNSPECIFIED.,.F.,.F.)
B_SPLINE_CURVE_WITH_KNOTS((3,3),(-3.98124427668322,-2.908605540086),
 .UNSPECIFIED.)
CURVE()
GEOMETRIC_REPRESENTATION_ITEM()
RATIONAL_B_SPLINE_CURVE((1.86639055127154,2.00276625701356,2.00276625701356))
REPRESENTATION_ITEM('')
);
#3204=(
BOUNDED_SURFACE()
B_SPLINE_SURFACE(1,2,((#309430,#309431,#309432,#309433,#309434,#309435,
#309436,#309437,#309438,#309439,#309440,#309441,#309442,#309443,#309444,
#309445,#309446,#309447,#309448,#309449,#309450,#309451,#309452,#309453,
#309454,#309455,#309456,#309457,#309458,#309459,#309460,#309461,#309462,
#309463,#309464,#309465,#309466,#309467,#309468,#309469,#309470,#309471,
#309472,#309473,#309474,#309475,#309476,#309477,#309478,#309479,#309480,
#309481,#309482,#309483,#309484,#309485,#309486,#309487,#309488,#309489,
#309490,#309491,#309492,#309493,#309494,#309495,#309496,#309497,#309498,
#309499,#309500,#309501,#309502,#309503,#309504,#309505,#309506,#309507,
#309508,#309509,#309510,#309511,#309512,#309513,#309514,#309515,#309516,
#309517,#309518,#309519,#309520,#309521,#309522,#309523,#309524,#309525,
#309526,#309527,#309528,#309529,#309530,#309531,#309532,#309533,#309534,
#309535,#309536,#309537,#309538,#309539,#309540,#309541,#309542,#309543,
#309544,#309545,#309546,#309547,#309548,#309549,#309550,#309551,#309552,
#309553,#309554,#309555,#309556,#309557,#309558,#309559,#309560,#309561,
#309562,#309563,#309564,#309565,#309566),(#309567,#309568,#309569,#309570,
#309571,#309572,#309573,#309574,#309575,#309576,#309577,#309578,#309579,
#309580,#309581,#309582,#309583,#309584,#309585,#309586,#309587,#309588,
#309589,#309590,#309591,#309592,#309593,#309594,#309595,#309596,#309597,
#309598,#309599,#309600,#309601,#309602,#309603,#309604,#309605,#309606,
#309607,#309608,#309609,#309610,#309611,#309612,#309613,#309614,#309615,
#309616,#309617,#309618,#309619,#309620,#309621,#309622,#309623,#309624,
#309625,#309626,#309627,#309628,#309629,#309630,#309631,#309632,#309633,
#309634,#309635,#309636,#309637,#309638,#309639,#309640,#309641,#309642,
#309643,#309644,#309645,#309646,#309647,#309648,#309649,#309650,#309651,
#309652,#309653,#309654,#309655,#309656,#309657,#309658,#309659,#309660,
#309661,#309662,#309663,#309664,#309665,#309666,#309667,#309668,#309669,
#309670,#309671,#309672,#309673,#309674,#309675,#309676,#309677,#309678,
#309679,#309680,#309681,#309682,#309683,#309684,#309685,#309686,#309687,
#309688,#309689,#309690,#309691,#309692,#309693,#309694,#309695,#309696,
#309697,#309698,#309699,#309700,#309701,#309702,#309703)),.UNSPECIFIED.,
 .F.,.F.,.F.)
B_SPLINE_SURFACE_WITH_KNOTS((2,2),(3,2,2,2,2,2,2,2,2,2,2,2,2,2,2,2,2,2,
2,2,2,2,2,2,2,2,2,2,2,2,2,2,2,2,2,2,2,2,2,2,2,2,2,2,2,2,2,2,2,2,2,2,2,2,
2,2,2,2,2,2,2,2,2,2,2,2,2,2,3),(0.,1.00001687186328),(0.,0.0142857142857143,
0.0285714285714285,0.0428571428571429,0.0571428571428571,0.0714285714285714,
0.0857142857142857,0.1,0.114285714285714,0.128571428571429,0.142857142857143,
0.157142857142857,0.171428571428572,0.185714285714285,0.2,0.214285714285714,
0.228571428571428,0.242857142857143,0.257142857142857,0.271428571428572,
0.285714285714286,0.3,0.314285714285715,0.328571428571429,0.342857142857143,
0.357142857142857,0.371428571428571,0.385714285714286,0.4,0.414285714285715,
0.428571428571428,0.442857142857143,0.457142857142857,0.471428571428571,
0.485714285714286,0.5,0.514285714285714,0.528571428571429,0.542857142857143,
0.557142857142857,0.571428571428571,0.585714285714286,0.6,0.614285714285714,
0.628571428571429,0.642857142857143,0.657142857142857,0.671428571428571,
0.685714285714286,0.7,0.714285714285714,0.728571428571428,0.742857142857143,
0.757142857142857,0.771428571428571,0.785714285714286,0.8,0.814285714285714,
0.828571428571429,0.842857142857143,0.857142857142857,0.871428571428571,
0.885714285714286,0.9,0.914285714285714,0.928571428571429,0.942857142857143,
0.957142857142857,0.95920445073468),.UNSPECIFIED.)
GEOMETRIC_REPRESENTATION_ITEM()
RATIONAL_B_SPLINE_SURFACE(((1.,0.951056516295154,1.,0.951056516295154,1.,
0.951056516295154,1.,0.951056516295154,1.,0.951056516295154,1.,0.951056516295154,
1.,0.951056516295154,1.,0.951056516295154,1.,0.951056516295154,1.,0.951056516295154,
1.,0.951056516295154,1.,0.951056516295154,1.,0.951056516295154,1.,0.951056516295154,
1.,0.951056516295154,1.,0.951056516295154,1.,0.951056516295154,1.,0.951056516295154,
1.,0.951056516295154,1.,0.951056516295154,1.,0.951056516295154,1.,0.951056516295154,
1.,0.951056516295154,1.,0.951056516295154,1.,0.951056516295154,1.,0.951056516295154,
1.,0.951056516295154,1.,0.951056516295154,1.,0.951056516295154,1.,0.951056516295154,
1.,0.951056516295154,1.,0.951056516295154,1.,0.951056516295154,1.,0.951056516295154,
1.,0.951056516295154,1.,0.951056516295154,1.,0.951056516295154,1.,0.951056516295154,
1.,0.951056516295154,1.,0.951056516295154,1.,0.951056516295154,1.,0.951056516295154,
1.,0.951056516295154,1.,0.951056516295154,1.,0.951056516295154,1.,0.951056516295154,
1.,0.951056516295154,1.,0.951056516295154,1.,0.951056516295154,1.,0.951056516295154,
1.,0.951056516295154,1.,0.951056516295154,1.,0.951056516295154,1.,0.951056516295154,
1.,0.951056516295154,1.,0.951056516295154,1.,0.951056516295154,1.,0.951056516295154,
1.,0.951056516295154,1.,0.951056516295154,1.,0.951056516295154,1.,0.951056516295154,
1.,0.951056516295154,1.,0.951056516295154,1.,0.951056516295154,1.,0.951056516295154,
1.,0.951056516295154,1.,0.99293688993428,0.987912356611537),(1.,0.951056516295154,
1.,0.951056516295154,1.,0.951056516295154,1.,0.951056516295154,1.,0.951056516295154,
1.,0.951056516295154,1.,0.951056516295154,1.,0.951056516295154,1.,0.951056516295154,
1.,0.951056516295154,1.,0.951056516295154,1.,0.951056516295154,1.,0.951056516295154,
1.,0.951056516295154,1.,0.951056516295154,1.,0.951056516295154,1.,0.951056516295154,
1.,0.951056516295154,1.,0.951056516295154,1.,0.951056516295154,1.,0.951056516295154,
1.,0.951056516295154,1.,0.951056516295154,1.,0.951056516295154,1.,0.951056516295154,
1.,0.951056516295154,1.,0.951056516295154,1.,0.951056516295154,1.,0.951056516295154,
1.,0.951056516295154,1.,0.951056516295154,1.,0.951056516295154,1.,0.951056516295154,
1.,0.951056516295154,1.,0.951056516295154,1.,0.951056516295154,1.,0.951056516295154,
1.,0.951056516295154,1.,0.951056516295154,1.,0.951056516295154,1.,0.951056516295154,
1.,0.951056516295154,1.,0.951056516295154,1.,0.951056516295154,1.,0.951056516295154,
1.,0.951056516295154,1.,0.951056516295154,1.,0.951056516295154,1.,0.951056516295154,
1.,0.951056516295154,1.,0.951056516295154,1.,0.951056516295154,1.,0.951056516295154,
1.,0.951056516295154,1.,0.951056516295154,1.,0.951056516295154,1.,0.951056516295154,
1.,0.951056516295154,1.,0.951056516295154,1.,0.951056516295154,1.,0.951056516295154,
1.,0.951056516295154,1.,0.951056516295154,1.,0.951056516295154,1.,0.951056516295154,
1.,0.951056516295154,1.,0.951056516295154,1.,0.99293688993428,0.987912356611537)))
REPRESENTATION_ITEM('')
SURFACE()
);
#3205=(
BOUNDED_SURFACE()
B_SPLINE_SURFACE(1,2,((#309842,#309843,#309844,#309845,#309846,#309847,
#309848,#309849,#309850,#309851,#309852,#309853,#309854,#309855,#309856,
#309857,#309858,#309859,#309860,#309861,#309862,#309863,#309864,#309865,
#309866,#309867,#309868,#309869,#309870,#309871,#309872,#309873,#309874,
#309875,#309876,#309877,#309878,#309879,#309880,#309881,#309882,#309883,
#309884,#309885,#309886,#309887,#309888,#309889,#309890,#309891,#309892,
#309893,#309894,#309895,#309896,#309897,#309898,#309899,#309900,#309901,
#309902,#309903,#309904,#309905,#309906,#309907,#309908,#309909,#309910,
#309911,#309912,#309913,#309914,#309915,#309916,#309917,#309918,#309919,
#309920,#309921,#309922,#309923,#309924,#309925,#309926,#309927,#309928,
#309929,#309930,#309931,#309932,#309933,#309934,#309935,#309936,#309937,
#309938,#309939,#309940,#309941,#309942,#309943,#309944,#309945,#309946,
#309947,#309948,#309949,#309950,#309951,#309952,#309953,#309954,#309955,
#309956,#309957,#309958,#309959,#309960,#309961,#309962,#309963,#309964,
#309965,#309966,#309967,#309968,#309969,#309970,#309971,#309972,#309973,
#309974,#309975,#309976,#309977,#309978),(#309979,#309980,#309981,#309982,
#309983,#309984,#309985,#309986,#309987,#309988,#309989,#309990,#309991,
#309992,#309993,#309994,#309995,#309996,#309997,#309998,#309999,#310000,
#310001,#310002,#310003,#310004,#310005,#310006,#310007,#310008,#310009,
#310010,#310011,#310012,#310013,#310014,#310015,#310016,#310017,#310018,
#310019,#310020,#310021,#310022,#310023,#310024,#310025,#310026,#310027,
#310028,#310029,#310030,#310031,#310032,#310033,#310034,#310035,#310036,
#310037,#310038,#310039,#310040,#310041,#310042,#310043,#310044,#310045,
#310046,#310047,#310048,#310049,#310050,#310051,#310052,#310053,#310054,
#310055,#310056,#310057,#310058,#310059,#310060,#310061,#310062,#310063,
#310064,#310065,#310066,#310067,#310068,#310069,#310070,#310071,#310072,
#310073,#310074,#310075,#310076,#310077,#310078,#310079,#310080,#310081,
#310082,#310083,#310084,#310085,#310086,#310087,#310088,#310089,#310090,
#310091,#310092,#310093,#310094,#310095,#310096,#310097,#310098,#310099,
#310100,#310101,#310102,#310103,#310104,#310105,#310106,#310107,#310108,
#310109,#310110,#310111,#310112,#310113,#310114,#310115)),.UNSPECIFIED.,
 .F.,.F.,.F.)
B_SPLINE_SURFACE_WITH_KNOTS((2,2),(3,2,2,2,2,2,2,2,2,2,2,2,2,2,2,2,2,2,
2,2,2,2,2,2,2,2,2,2,2,2,2,2,2,2,2,2,2,2,2,2,2,2,2,2,2,2,2,2,2,2,2,2,2,2,
2,2,2,2,2,2,2,2,2,2,2,2,2,2,3),(-5.49146708075157E-6,1.),(0.,0.0142857142857143,
0.0285714285714285,0.0428571428571429,0.0571428571428571,0.0714285714285714,
0.0857142857142857,0.1,0.114285714285714,0.128571428571429,0.142857142857143,
0.157142857142857,0.171428571428572,0.185714285714285,0.2,0.214285714285714,
0.228571428571428,0.242857142857143,0.257142857142857,0.271428571428572,
0.285714285714286,0.3,0.314285714285715,0.328571428571429,0.342857142857143,
0.357142857142857,0.371428571428571,0.385714285714286,0.4,0.414285714285715,
0.428571428571428,0.442857142857143,0.457142857142857,0.471428571428571,
0.485714285714286,0.5,0.514285714285714,0.528571428571429,0.542857142857143,
0.557142857142857,0.571428571428571,0.585714285714286,0.6,0.614285714285714,
0.628571428571429,0.642857142857143,0.657142857142857,0.671428571428571,
0.685714285714286,0.7,0.714285714285714,0.728571428571428,0.742857142857143,
0.757142857142857,0.771428571428571,0.785714285714286,0.8,0.814285714285714,
0.828571428571429,0.842857142857143,0.857142857142857,0.871428571428571,
0.885714285714286,0.9,0.914285714285714,0.928571428571429,0.942857142857143,
0.957142857142857,0.959204499671976),.UNSPECIFIED.)
GEOMETRIC_REPRESENTATION_ITEM()
RATIONAL_B_SPLINE_SURFACE(((1.,0.951056516295154,1.,0.951056516295154,1.,
0.951056516295154,1.,0.951056516295154,1.,0.951056516295154,1.,0.951056516295154,
1.,0.951056516295154,1.,0.951056516295154,1.,0.951056516295154,1.,0.951056516295154,
1.,0.951056516295154,1.,0.951056516295154,1.,0.951056516295154,1.,0.951056516295154,
1.,0.951056516295154,1.,0.951056516295154,1.,0.951056516295154,1.,0.951056516295154,
1.,0.951056516295154,1.,0.951056516295154,1.,0.951056516295154,1.,0.951056516295154,
1.,0.951056516295154,1.,0.951056516295154,1.,0.951056516295154,1.,0.951056516295154,
1.,0.951056516295154,1.,0.951056516295154,1.,0.951056516295154,1.,0.951056516295154,
1.,0.951056516295154,1.,0.951056516295154,1.,0.951056516295154,1.,0.951056516295154,
1.,0.951056516295154,1.,0.951056516295154,1.,0.951056516295154,1.,0.951056516295154,
1.,0.951056516295154,1.,0.951056516295154,1.,0.951056516295154,1.,0.951056516295154,
1.,0.951056516295154,1.,0.951056516295154,1.,0.951056516295154,1.,0.951056516295154,
1.,0.951056516295154,1.,0.951056516295154,1.,0.951056516295154,1.,0.951056516295154,
1.,0.951056516295154,1.,0.951056516295154,1.,0.951056516295154,1.,0.951056516295154,
1.,0.951056516295154,1.,0.951056516295154,1.,0.951056516295154,1.,0.951056516295154,
1.,0.951056516295154,1.,0.951056516295154,1.,0.951056516295154,1.,0.951056516295154,
1.,0.951056516295154,1.,0.951056516295154,1.,0.951056516295154,1.,0.951056516295154,
1.,0.951056516295154,1.,0.992936722272959,0.987912118071905),(1.,0.951056516295154,
1.,0.951056516295154,1.,0.951056516295154,1.,0.951056516295154,1.,0.951056516295154,
1.,0.951056516295154,1.,0.951056516295154,1.,0.951056516295154,1.,0.951056516295154,
1.,0.951056516295154,1.,0.951056516295154,1.,0.951056516295154,1.,0.951056516295154,
1.,0.951056516295154,1.,0.951056516295154,1.,0.951056516295154,1.,0.951056516295154,
1.,0.951056516295154,1.,0.951056516295154,1.,0.951056516295154,1.,0.951056516295154,
1.,0.951056516295154,1.,0.951056516295154,1.,0.951056516295154,1.,0.951056516295154,
1.,0.951056516295154,1.,0.951056516295154,1.,0.951056516295154,1.,0.951056516295154,
1.,0.951056516295154,1.,0.951056516295154,1.,0.951056516295154,1.,0.951056516295154,
1.,0.951056516295154,1.,0.951056516295154,1.,0.951056516295154,1.,0.951056516295154,
1.,0.951056516295154,1.,0.951056516295154,1.,0.951056516295154,1.,0.951056516295154,
1.,0.951056516295154,1.,0.951056516295154,1.,0.951056516295154,1.,0.951056516295154,
1.,0.951056516295154,1.,0.951056516295154,1.,0.951056516295154,1.,0.951056516295154,
1.,0.951056516295154,1.,0.951056516295154,1.,0.951056516295154,1.,0.951056516295154,
1.,0.951056516295154,1.,0.951056516295154,1.,0.951056516295154,1.,0.951056516295154,
1.,0.951056516295154,1.,0.951056516295154,1.,0.951056516295154,1.,0.951056516295154,
1.,0.951056516295154,1.,0.951056516295154,1.,0.951056516295154,1.,0.951056516295154,
1.,0.951056516295154,1.,0.951056516295154,1.,0.992936722272959,0.987912118071905)))
REPRESENTATION_ITEM('')
SURFACE()
);
#6898=B_SPLINE_CURVE_WITH_KNOTS('',3,(#308953,#308954,#308955,#308956,#308957,
#308958,#308959,#308960),.UNSPECIFIED.,.F.,.F.,(4,2,2,4),(9.9999999767032E-7,
0.0999956551432425,0.200882472133143,0.263234170060192),.UNSPECIFIED.);
#6899=B_SPLINE_CURVE_WITH_KNOTS('',3,(#308963,#308964,#308965,#308966,#308967,
#308968,#308969,#308970,#308971,#308972,#308973,#308974,#308975,#308976),
 .UNSPECIFIED.,.F.,.F.,(4,2,2,2,2,2,4),(0.173683564667831,0.259058622119751,
0.290413783825993,0.354637717539737,0.477856124224731,0.523001497040519,
0.557151695094327),.UNSPECIFIED.);
#6900=B_SPLINE_CURVE_WITH_KNOTS('',3,(#308982,#308983,#308984,#308985,#308986,
#308987,#308988,#308989,#308990,#308991,#308992,#308993,#308994,#308995,
#308996,#308997),.UNSPECIFIED.,.F.,.F.,(4,2,2,2,2,2,2,4),(-18.6044232501874,
-18.4152204113709,-18.2260245198036,-17.9923887330122,-17.7587449034554,
-17.5216133328485,-17.2892573593602,-17.2798161593979),.UNSPECIFIED.);
#6901=B_SPLINE_CURVE_WITH_KNOTS('',3,(#309000,#309001,#309002,#309003,#309004,
#309005,#309006,#309007,#309008,#309009,#309010,#309011,#309012,#309013,
#309014,#309015,#309016,#309017,#309018,#309019),.UNSPECIFIED.,.F.,.F.,
(4,2,2,2,2,2,2,2,2,4),(-1.79914710673844,-1.71083038040228,-1.47755135902926,
-1.24339398648431,-1.00520383669562,-0.772910845791891,-0.536812809995226,
-0.301993255983215,-0.150081981195142,-1.00000002722922E-6),
 .UNSPECIFIED.);
#6902=B_SPLINE_CURVE_WITH_KNOTS('',3,(#309024,#309025,#309026,#309027,#309028,
#309029,#309030,#309031,#309032,#309033,#309034,#309035,#309036,#309037,
#309038,#309039,#309040,#309041,#309042,#309043,#309044,#309045,#309046,
#309047,#309048,#309049,#309050,#309051,#309052,#309053,#309054,#309055,
#309056,#309057,#309058,#309059),.UNSPECIFIED.,.F.,.F.,(4,2,2,2,2,2,2,2,
2,2,2,2,2,2,2,2,2,4),(-17.2798161593979,-17.052938737066,-16.8178352897546,
-16.5852392730586,-16.3465740061095,-16.1134283553821,-15.8792563449518,
-15.6427035707161,-15.4104662708811,-15.1732497436008,-14.9386827923542,
-14.7058108627647,-14.4677107158127,-14.2349546508748,-14.0001041866954,
-13.7640911714114,-13.5318263968762,-13.4939982929491),.UNSPECIFIED.);
#6903=B_SPLINE_CURVE_WITH_KNOTS('',3,(#309060,#309061,#309062,#309063,#309064,
#309065,#309066,#309067,#309068,#309069,#309070,#309071,#309072,#309073,
#309074,#309075,#309076,#309077,#309078,#309079,#309080,#309081,#309082,
#309083,#309084,#309085,#309086,#309087,#309088,#309089,#309090,#309091,
#309092,#309093,#309094,#309095),.UNSPECIFIED.,.F.,.F.,(4,2,2,2,2,2,2,2,
2,2,2,2,2,2,2,2,2,4),(-5.58533174762334,-5.47049549570421,-5.23630005753687,
-5.00320609709793,-4.76460194975688,-4.53201074387952,-4.29696593781882,
-4.06060911752499,-3.82828546976905,-3.59121525458418,-3.35755892023313,
-3.12394708830492,-2.88474500970487,-2.65229456245123,-2.41668456425235,
-2.18107128571481,-1.94850078969714,-1.79914710673844),.UNSPECIFIED.);
#6904=B_SPLINE_CURVE_WITH_KNOTS('',3,(#309100,#309101,#309102,#309103,#309104,
#309105,#309106,#309107,#309108,#309109,#309110,#309111,#309112,#309113,
#309114,#309115,#309116,#309117,#309118,#309119,#309120,#309121,#309122,
#309123,#309124,#309125,#309126,#309127,#309128,#309129,#309130,#309131,
#309132,#309133,#309134,#309135),.UNSPECIFIED.,.F.,.F.,(4,2,2,2,2,2,2,2,
2,2,2,2,2,2,2,2,2,4),(-13.4939982929491,-13.2935738952139,-13.0594962824575,
-12.82621091684,-12.5886227052581,-12.3561047086897,-12.1204506023339,-11.8849195874974,
-11.6524849000808,-11.4133654689514,-11.1798323235161,-10.9461539830993,
-10.7091643355172,-10.4768804983775,-10.2404660644835,-10.0054978175092,
-9.77290831091157,-9.70804701379833),.UNSPECIFIED.);
#6905=B_SPLINE_CURVE_WITH_KNOTS('',3,(#309136,#309137,#309138,#309139,#309140,
#309141,#309142,#309143,#309144,#309145,#309146,#309147,#309148,#309149,
#309150,#309151,#309152,#309153,#309154,#309155,#309156,#309157,#309158,
#309159,#309160,#309161,#309162,#309163,#309164,#309165,#309166,#309167,
#309168,#309169,#309170,#309171),.UNSPECIFIED.,.F.,.F.,(4,2,2,2,2,2,2,2,
2,2,2,2,2,2,2,2,2,4),(-9.37108296243015,-9.22906033338744,-8.99336556927607,
-8.76087801275906,-8.5233432522494,-8.29004361701075,-8.0560178270479,-7.81770817391695,
-7.58545544178997,-7.34949823768963,-7.11461462448207,-6.88189986296259,
-6.64385766283799,-6.41098047501652,-6.17646937131389,-5.93920391259217,
-5.70698895911159,-5.58533174762334),.UNSPECIFIED.);
#6906=B_SPLINE_CURVE_WITH_KNOTS('',3,(#309176,#309177,#309178,#309179,#309180,
#309181,#309182,#309183,#309184,#309185,#309186,#309187,#309188,#309189,
#309190,#309191,#309192,#309193,#309194,#309195,#309196,#309197,#309198,
#309199,#309200,#309201,#309202,#309203,#309204,#309205,#309206,#309207,
#309208,#309209,#309210,#309211),.UNSPECIFIED.,.F.,.F.,(4,2,2,2,2,2,2,2,
2,2,2,2,2,2,2,2,2,4),(-9.70804701379833,-9.5343840344758,-9.30135623596084,
-9.06916727008946,-8.83282972254009,-8.59850286837222,-8.36553560893589,
-8.12709334075291,-7.8944679782875,-7.65957741824112,-7.42303753393001,
-7.19077496732653,-6.95386883099392,-6.7201187307232,-6.48666520198793,
-6.2476321327511,-6.01518268074078,-5.9226637994781),.UNSPECIFIED.);
#6907=B_SPLINE_CURVE_WITH_KNOTS('',3,(#309212,#309213,#309214,#309215,#309216,
#309217,#309218,#309219,#309220,#309221,#309222,#309223,#309224,#309225,
#309226,#309227,#309228,#309229,#309230,#309231,#309232,#309233,#309234,
#309235,#309236,#309237,#309238,#309239,#309240,#309241,#309242,#309243,
#309244,#309245,#309246,#309247),.UNSPECIFIED.,.F.,.F.,(4,2,2,2,2,2,2,2,
2,2,2,2,2,2,2,2,2,4),(-13.1564141152525,-12.9837710456499,-12.7507729137427,
-12.516492005001,-12.2801143778626,-12.0479245003057,-11.8105120712351,
-11.5761085159543,-11.3431900419091,-11.1052599297713,-10.872615747501,
-10.6376237109982,-10.4017735871133,-10.1695212094451,-9.93603831046464,
-9.6969725154889,-9.46454033645112,-9.37108296243015),.UNSPECIFIED.);
#6908=B_SPLINE_CURVE_WITH_KNOTS('',3,(#309253,#309254,#309255,#309256,#309257,
#309258,#309259,#309260,#309261,#309262,#309263,#309264,#309265,#309266,
#309267,#309268,#309269,#309270),.UNSPECIFIED.,.F.,.F.,(4,2,2,2,2,2,2,2,
4),(-18.6041766476204,-18.3879254158768,-18.1550376114361,-17.9169842730623,
-17.6842586928035,-17.4493644967635,-17.2133962593625,-16.9811328612893,
-16.9423174515002),.UNSPECIFIED.);
#6909=B_SPLINE_CURVE_WITH_KNOTS('',3,(#309275,#309276,#309277,#309278,#309279,
#309280,#309281,#309282,#309283,#309284,#309285,#309286,#309287,#309288,
#309289,#309290,#309291,#309292,#309293,#309294,#309295,#309296),
 .UNSPECIFIED.,.F.,.F.,(4,2,2,2,2,2,2,2,2,2,4),(-2.13687759585315,-2.0210882487643,
-1.78684984563254,-1.55378702616903,-1.31522335637624,-1.08261714125924,
-0.847610685706001,-0.611196108780494,-0.37888477337317,-0.188471738845002,
-9.99999997475243E-7),.UNSPECIFIED.);
#6910=B_SPLINE_CURVE_WITH_KNOTS('',3,(#309704,#309705,#309706,#309707,#309708,
#309709,#309710,#309711,#309712,#309713,#309714,#309715,#309716,#309717,
#309718,#309719,#309720,#309721,#309722,#309723,#309724,#309725,#309726,
#309727,#309728,#309729,#309730,#309731,#309732,#309733,#309734,#309735,
#309736,#309737,#309738,#309739),.UNSPECIFIED.,.F.,.F.,(4,2,2,2,2,2,2,2,
2,2,2,2,2,2,2,2,2,4),(-5.9226637994781,-5.77973314889478,-5.54397852289478,
-5.3115010616718,-5.07399902404122,-4.84066556806495,-4.6066712207202,-4.36828521464463,
-4.13602452995896,-3.90010256975103,-3.66516638126514,-3.43247239015531,
-3.19446738741631,-2.96156518684184,-2.72708953409623,-2.48975570213967,
-2.25754292115493,-2.13687759585315),.UNSPECIFIED.);
#6911=B_SPLINE_CURVE_WITH_KNOTS('',3,(#309740,#309741,#309742,#309743,#309744,
#309745),.UNSPECIFIED.,.F.,.F.,(4,2,4),(9.99997409965433E-7,0.146501658577725,
0.173683564667831),.UNSPECIFIED.);
#6912=B_SPLINE_CURVE_WITH_KNOTS('',3,(#309768,#309769,#309770,#309771,#309772,
#309773,#309774,#309775,#309776,#309777,#309778,#309779,#309780,#309781,
#309782,#309783,#309784,#309785,#309786,#309787,#309788,#309789,#309790,
#309791,#309792,#309793,#309794,#309795,#309796,#309797),.UNSPECIFIED.,
 .F.,.F.,(4,2,2,2,2,2,2,2,2,2,2,2,2,2,4),(9.99999999726749E-7,0.130707839264569,
0.259991147819482,0.472998818331275,0.696716416745347,0.814147340124016,
1.04649848427486,1.30651726561565,1.57149762551086,1.7131254536093,1.85156786432642,
2.15668396285832,2.483222578382,2.64892396867161,2.83146336233688),
 .UNSPECIFIED.);
#6913=B_SPLINE_CURVE_WITH_KNOTS('',3,(#309798,#309799,#309800,#309801,#309802,
#309803,#309804,#309805,#309806,#309807,#309808,#309809,#309810,#309811,
#309812,#309813,#309814,#309815,#309816,#309817),.UNSPECIFIED.,.F.,.F.,
(4,2,2,2,2,2,2,2,2,4),(2.83146336233688,2.98157423495795,3.32273775251514,
3.49495675413182,3.87338751477843,4.28823841167863,4.37710950869524,4.68170098346783,
4.83417108518993,4.99060309891423),.UNSPECIFIED.);
#6914=B_SPLINE_CURVE_WITH_KNOTS('',3,(#310116,#310117,#310118,#310119,#310120,
#310121,#310122,#310123,#310124,#310125,#310126,#310127,#310128,#310129,
#310130,#310131,#310132,#310133,#310134,#310135,#310136,#310137,#310138,
#310139,#310140,#310141,#310142,#310143,#310144,#310145,#310146,#310147,
#310148,#310149,#310150,#310151,#310152,#310153,#310154,#310155,#310156,
#310157),.UNSPECIFIED.,.F.,.F.,(4,2,2,2,2,2,2,2,2,2,2,2,2,2,2,2,2,2,2,2,
4),(0.263234170060192,0.387368656471732,0.436487962699596,0.633460506504842,
0.855015445306774,0.974732004315266,1.24137222287131,1.52351378413127,1.67243408083146,
1.96519939944981,2.28406876404804,2.45461478920459,2.83048775636771,3.24439250987047,
3.34640175008835,3.7582012400543,4.2159969589176,4.71750949992909,4.90457358104075,
5.17859562204822,5.45614014826222),.UNSPECIFIED.);
#6915=B_SPLINE_CURVE_WITH_KNOTS('',3,(#310158,#310159,#310160,#310161,#310162,
#310163,#310164,#310165,#310166,#310167,#310168,#310169,#310170,#310171,
#310172,#310173,#310174,#310175,#310176,#310177,#310178,#310179,#310180,
#310181,#310182,#310183,#310184,#310185,#310186,#310187,#310188,#310189,
#310190,#310191,#310192,#310193),.UNSPECIFIED.,.F.,.F.,(4,2,2,2,2,2,2,2,
2,2,2,2,2,2,2,2,2,4),(-16.9423174515002,-16.7428124565089,-16.5087755987168,
-16.2754652275235,-16.0379192294675,-15.8054207736165,-15.5697152811951,
-15.3342241467486,-15.1017811964504,-14.8627040923319,-14.6292101590594,
-14.3954948845505,-14.1585461493712,-13.9262721968018,-13.6897937684499,
-13.4548635315576,-13.2222551407783,-13.1564141152525),.UNSPECIFIED.);
#6916=B_SPLINE_CURVE_WITH_KNOTS('',3,(#310194,#310195,#310196,#310197,#310198,
#310199,#310200,#310201,#310202,#310203,#310204,#310205,#310206,#310207,
#310208,#310209),.UNSPECIFIED.,.F.,.F.,(4,2,2,2,2,2,2,4),(9.99998665002523E-7,
0.17925540834401,0.324372801233075,0.360565347733573,0.497288613301502,
0.54664963487918,0.61356551678679,0.671648570926337),.UNSPECIFIED.);
#6917=B_SPLINE_CURVE_WITH_KNOTS('',3,(#310213,#310214,#310215,#310216,#310217,
#310218,#310219,#310220,#310221,#310222),.UNSPECIFIED.,.F.,.F.,(4,2,2,2,
4),(-0.0616936784912174,-0.0584304026796343,-0.0471362732342459,-0.0358421437888575,
-0.0325788679773239),.UNSPECIFIED.);
#6918=B_SPLINE_CURVE_WITH_KNOTS('',3,(#310226,#310227,#310228,#310229,#310230,
#310231,#310232,#310233,#310234,#310235),.UNSPECIFIED.,.F.,.F.,(4,2,2,2,
4),(-0.152743320152561,-0.149480044341046,-0.138185914895657,-0.126891785450269,
-0.123628509639395),.UNSPECIFIED.);
#6919=B_SPLINE_CURVE_WITH_KNOTS('',3,(#310240,#310241,#310242,#310243,#310244,
#310245,#310246,#310247,#310248,#310249),.UNSPECIFIED.,.F.,.F.,(4,2,2,2,
4),(-0.0616936784912628,-0.0584304026796342,-0.0471362732342458,-0.0358421437888575,
-0.0325788679773241),.UNSPECIFIED.);
#6920=B_SPLINE_CURVE_WITH_KNOTS('',3,(#310253,#310254,#310255,#310256,#310257,
#310258,#310259,#310260,#310261,#310262),.UNSPECIFIED.,.F.,.F.,(4,2,2,2,
4),(-0.152743320152561,-0.149480044341046,-0.138185914895657,-0.126891785450269,
-0.123628509639806),.UNSPECIFIED.);
#6921=B_SPLINE_CURVE_WITH_KNOTS('',3,(#310267,#310268,#310269,#310270,#310271,
#310272,#310273,#310274,#310275,#310276),.UNSPECIFIED.,.F.,.F.,(4,2,2,2,
4),(-0.061693678491264,-0.0584304026796342,-0.0471362732342458,-0.0358421437888574,
-0.0325788679773307),.UNSPECIFIED.);
#6922=B_SPLINE_CURVE_WITH_KNOTS('',3,(#310280,#310281,#310282,#310283,#310284,
#310285,#310286,#310287,#310288,#310289),.UNSPECIFIED.,.F.,.F.,(4,2,2,2,
4),(-0.152743320152482,-0.149480044341046,-0.138185914895657,-0.126891785450269,
-0.123628509639806),.UNSPECIFIED.);
#6923=B_SPLINE_CURVE_WITH_KNOTS('',3,(#310294,#310295,#310296,#310297,#310298,
#310299,#310300,#310301,#310302,#310303),.UNSPECIFIED.,.F.,.F.,(4,2,2,2,
4),(-0.0616936784912173,-0.0584304026796343,-0.0471362732342459,-0.0358421437888575,
-0.032578867977324),.UNSPECIFIED.);
#6924=B_SPLINE_CURVE_WITH_KNOTS('',3,(#310307,#310308,#310309,#310310,#310311,
#310312,#310313,#310314,#310315,#310316),.UNSPECIFIED.,.F.,.F.,(4,2,2,2,
4),(-0.152743320152561,-0.149480044341046,-0.138185914895657,-0.126891785450269,
-0.123628509639395),.UNSPECIFIED.);
#6925=B_SPLINE_CURVE_WITH_KNOTS('',3,(#310321,#310322,#310323,#310324,#310325,
#310326,#310327,#310328,#310329,#310330),.UNSPECIFIED.,.F.,.F.,(4,2,2,2,
4),(-0.0616936784912626,-0.0584304026796342,-0.0471362732342458,-0.0358421437888574,
-0.032578867977324),.UNSPECIFIED.);
#6926=B_SPLINE_CURVE_WITH_KNOTS('',3,(#310334,#310335,#310336,#310337,#310338,
#310339,#310340,#310341,#310342,#310343),.UNSPECIFIED.,.F.,.F.,(4,2,2,2,
4),(-0.152743320152561,-0.149480044341046,-0.138185914895657,-0.126891785450269,
-0.123628509639806),.UNSPECIFIED.);
#6927=B_SPLINE_CURVE_WITH_KNOTS('',3,(#310348,#310349,#310350,#310351,#310352,
#310353,#310354,#310355,#310356,#310357),.UNSPECIFIED.,.F.,.F.,(4,2,2,2,
4),(-0.0616936784912639,-0.0584304026796342,-0.0471362732342458,-0.0358421437888574,
-0.0325788679773305),.UNSPECIFIED.);
#6928=B_SPLINE_CURVE_WITH_KNOTS('',3,(#310361,#310362,#310363,#310364,#310365,
#310366,#310367,#310368,#310369,#310370),.UNSPECIFIED.,.F.,.F.,(4,2,2,2,
4),(-0.152743320152481,-0.149480044341046,-0.138185914895657,-0.126891785450269,
-0.123628509639806),.UNSPECIFIED.);
#7207=CONICAL_SURFACE('',#104721,6.,0.785398163397452);
#7208=CONICAL_SURFACE('',#104744,9.5,1.0471975511966);
#7209=CONICAL_SURFACE('',#104746,9.5,1.0471975511966);
#7210=CONICAL_SURFACE('',#104748,9.5,1.0471975511966);
#7211=CONICAL_SURFACE('',#104750,9.5,1.0471975511966);
#7212=CONICAL_SURFACE('',#104752,9.5,1.0471975511966);
#7213=CONICAL_SURFACE('',#104754,9.5,1.0471975511966);
#7214=CONICAL_SURFACE('',#104756,9.5,1.0471975511966);
#7215=CONICAL_SURFACE('',#104758,9.5,1.0471975511966);
#7216=CONICAL_SURFACE('',#104760,9.5,1.0471975511966);
#7217=CONICAL_SURFACE('',#104762,9.5,1.0471975511966);
#7218=CONICAL_SURFACE('',#104764,9.5,1.0471975511966);
#7219=CONICAL_SURFACE('',#104766,9.5,1.0471975511966);
#7220=CONICAL_SURFACE('',#104779,6.7,0.785398163397448);
#7221=CONICAL_SURFACE('',#104780,6.,0.785398163397452);
#7238=SHAPE_REPRESENTATION_RELATIONSHIP('SRR','None',#310913,#7255);
#7255=ADVANCED_BREP_SHAPE_REPRESENTATION('',(#7390),#310622);
#7323=STYLED_ITEM('',(#311008),#7390);
#7390=MANIFOLD_SOLID_BREP('Body1',#93774);
#7704=FACE_BOUND('',#20476,.T.);
#7705=FACE_BOUND('',#20478,.T.);
#8680=PLANE('',#104769);
#8681=PLANE('',#104770);
#8682=PLANE('',#104771);
#8683=PLANE('',#104772);
#8684=PLANE('',#104773);
#8685=PLANE('',#104774);
#8686=PLANE('',#104775);
#8687=PLANE('',#104777);
#14385=FACE_OUTER_BOUND('',#20437,.T.);
#14386=FACE_OUTER_BOUND('',#20438,.T.);
#14387=FACE_OUTER_BOUND('',#20439,.T.);
#14388=FACE_OUTER_BOUND('',#20440,.T.);
#14389=FACE_OUTER_BOUND('',#20441,.T.);
#14390=FACE_OUTER_BOUND('',#20442,.T.);
#14391=FACE_OUTER_BOUND('',#20443,.T.);
#14392=FACE_OUTER_BOUND('',#20444,.T.);
#14393=FACE_OUTER_BOUND('',#20445,.T.);
#14394=FACE_OUTER_BOUND('',#20446,.T.);
#14395=FACE_OUTER_BOUND('',#20447,.T.);
#14396=FACE_OUTER_BOUND('',#20448,.T.);
#14397=FACE_OUTER_BOUND('',#20449,.T.);
#14398=FACE_OUTER_BOUND('',#20450,.T.);
#14399=FACE_OUTER_BOUND('',#20451,.T.);
#14400=FACE_OUTER_BOUND('',#20452,.T.);
#14401=FACE_OUTER_BOUND('',#20453,.T.);
#14402=FACE_OUTER_BOUND('',#20454,.T.);
#14403=FACE_OUTER_BOUND('',#20455,.T.);
#14404=FACE_OUTER_BOUND('',#20456,.T.);
#14405=FACE_OUTER_BOUND('',#20457,.T.);
#14406=FACE_OUTER_BOUND('',#20458,.T.);
#14407=FACE_OUTER_BOUND('',#20459,.T.);
#14408=FACE_OUTER_BOUND('',#20460,.T.);
#14409=FACE_OUTER_BOUND('',#20461,.T.);
#14410=FACE_OUTER_BOUND('',#20462,.T.);
#14411=FACE_OUTER_BOUND('',#20463,.T.);
#14412=FACE_OUTER_BOUND('',#20464,.T.);
#14413=FACE_OUTER_BOUND('',#20465,.T.);
#14414=FACE_OUTER_BOUND('',#20466,.T.);
#14415=FACE_OUTER_BOUND('',#20467,.T.);
#14416=FACE_OUTER_BOUND('',#20468,.T.);
#14417=FACE_OUTER_BOUND('',#20469,.T.);
#14418=FACE_OUTER_BOUND('',#20470,.T.);
#14419=FACE_OUTER_BOUND('',#20471,.T.);
#14420=FACE_OUTER_BOUND('',#20472,.T.);
#14421=FACE_OUTER_BOUND('',#20473,.T.);
#14422=FACE_OUTER_BOUND('',#20474,.T.);
#14423=FACE_OUTER_BOUND('',#20475,.T.);
#14424=FACE_OUTER_BOUND('',#20477,.T.);
#14425=FACE_OUTER_BOUND('',#20479,.T.);
#14426=FACE_OUTER_BOUND('',#20480,.T.);
#20437=EDGE_LOOP('',(#85539,#85540,#85541,#85542));
#20438=EDGE_LOOP('',(#85543,#85544,#85545,#85546));
#20439=EDGE_LOOP('',(#85547,#85548,#85549,#85550));
#20440=EDGE_LOOP('',(#85551,#85552,#85553,#85554));
#20441=EDGE_LOOP('',(#85555,#85556,#85557,#85558));
#20442=EDGE_LOOP('',(#85559,#85560,#85561,#85562,#85563));
#20443=EDGE_LOOP('',(#85564,#85565,#85566,#85567));
#20444=EDGE_LOOP('',(#85568,#85569,#85570,#85571));
#20445=EDGE_LOOP('',(#85572,#85573,#85574,#85575));
#20446=EDGE_LOOP('',(#85576,#85577,#85578));
#20447=EDGE_LOOP('',(#85579,#85580,#85581,#85582,#85583,#85584,#85585,#85586,
#85587,#85588,#85589,#85590,#85591,#85592,#85593));
#20448=EDGE_LOOP('',(#85594,#85595,#85596,#85597,#85598));
#20449=EDGE_LOOP('',(#85599,#85600,#85601,#85602,#85603,#85604,#85605,#85606,
#85607,#85608,#85609,#85610,#85611));
#20450=EDGE_LOOP('',(#85612,#85613,#85614,#85615));
#20451=EDGE_LOOP('',(#85616,#85617,#85618,#85619));
#20452=EDGE_LOOP('',(#85620,#85621,#85622,#85623));
#20453=EDGE_LOOP('',(#85624,#85625,#85626,#85627));
#20454=EDGE_LOOP('',(#85628,#85629,#85630,#85631));
#20455=EDGE_LOOP('',(#85632,#85633,#85634,#85635));
#20456=EDGE_LOOP('',(#85636,#85637,#85638,#85639));
#20457=EDGE_LOOP('',(#85640,#85641,#85642,#85643));
#20458=EDGE_LOOP('',(#85644,#85645,#85646,#85647));
#20459=EDGE_LOOP('',(#85648,#85649,#85650,#85651));
#20460=EDGE_LOOP('',(#85652,#85653,#85654,#85655));
#20461=EDGE_LOOP('',(#85656,#85657,#85658,#85659));
#20462=EDGE_LOOP('',(#85660,#85661,#85662,#85663));
#20463=EDGE_LOOP('',(#85664,#85665,#85666,#85667));
#20464=EDGE_LOOP('',(#85668,#85669,#85670,#85671));
#20465=EDGE_LOOP('',(#85672,#85673,#85674,#85675));
#20466=EDGE_LOOP('',(#85676,#85677,#85678,#85679));
#20467=EDGE_LOOP('',(#85680,#85681,#85682,#85683));
#20468=EDGE_LOOP('',(#85684,#85685,#85686,#85687));
#20469=EDGE_LOOP('',(#85688,#85689,#85690,#85691,#85692,#85693));
#20470=EDGE_LOOP('',(#85694,#85695,#85696,#85697,#85698,#85699));
#20471=EDGE_LOOP('',(#85700,#85701,#85702,#85703,#85704,#85705));
#20472=EDGE_LOOP('',(#85706,#85707,#85708,#85709,#85710,#85711));
#20473=EDGE_LOOP('',(#85712,#85713,#85714,#85715,#85716,#85717));
#20474=EDGE_LOOP('',(#85718,#85719,#85720,#85721,#85722,#85723));
#20475=EDGE_LOOP('',(#85724,#85725,#85726,#85727,#85728,#85729));
#20476=EDGE_LOOP('',(#85730));
#20477=EDGE_LOOP('',(#85731,#85732,#85733,#85734,#85735,#85736));
#20478=EDGE_LOOP('',(#85737));
#20479=EDGE_LOOP('',(#85738,#85739,#85740,#85741,#85742,#85743,#85744,#85745,
#85746));
#20480=EDGE_LOOP('',(#85747,#85748,#85749,#85750,#85751,#85752,#85753,#85754));
#24804=LINE('',#308951,#29151);
#24805=LINE('',#308980,#29152);
#24806=LINE('',#309023,#29153);
#24807=LINE('',#309099,#29154);
#24808=LINE('',#309175,#29155);
#24809=LINE('',#309251,#29156);
#24810=LINE('',#309300,#29157);
#24811=LINE('',#309332,#29158);
#24812=LINE('',#309378,#29159);
#24813=LINE('',#309424,#29160);
#24814=LINE('',#310224,#29161);
#24815=LINE('',#310236,#29162);
#24816=LINE('',#310251,#29163);
#24817=LINE('',#310263,#29164);
#24818=LINE('',#310278,#29165);
#24819=LINE('',#310290,#29166);
#24820=LINE('',#310305,#29167);
#24821=LINE('',#310317,#29168);
#24822=LINE('',#310332,#29169);
#24823=LINE('',#310344,#29170);
#24824=LINE('',#310359,#29171);
#24825=LINE('',#310371,#29172);
#24826=LINE('',#310494,#29173);
#24827=LINE('',#310496,#29174);
#29151=VECTOR('',#130705,6.);
#29152=VECTOR('',#130710,6.);
#29153=VECTOR('',#130715,6.);
#29154=VECTOR('',#130718,6.);
#29155=VECTOR('',#130721,6.);
#29156=VECTOR('',#130724,6.);
#29157=VECTOR('',#130731,4.86334165753295);
#29158=VECTOR('',#130734,4.86334165753295);
#29159=VECTOR('',#130737,4.86334165753295);
#29160=VECTOR('',#130740,4.86334165753295);
#29161=VECTOR('',#130749,1000.);
#29162=VECTOR('',#130750,1000.);
#29163=VECTOR('',#130753,1000.);
#29164=VECTOR('',#130754,1000.);
#29165=VECTOR('',#130757,1000.);
#29166=VECTOR('',#130758,1000.);
#29167=VECTOR('',#130761,1000.);
#29168=VECTOR('',#130762,1000.);
#29169=VECTOR('',#130765,1000.);
#29170=VECTOR('',#130766,1000.);
#29171=VECTOR('',#130769,1000.);
#29172=VECTOR('',#130770,1000.);
#29173=VECTOR('',#130843,6.7);
#29174=VECTOR('',#130846,6.);
#35085=CIRCLE('',#104722,4.86334165753295);
#35086=CIRCLE('',#104724,6.);
#35087=CIRCLE('',#104729,6.);
#35088=CIRCLE('',#104730,6.);
#35089=CIRCLE('',#104735,4.86334165753295);
#35090=CIRCLE('',#104737,4.86334165753295);
#35091=CIRCLE('',#104745,9.5);
#35092=CIRCLE('',#104747,9.5);
#35093=CIRCLE('',#104749,9.5);
#35094=CIRCLE('',#104751,9.5);
#35095=CIRCLE('',#104753,9.5);
#35096=CIRCLE('',#104755,9.5);
#35097=CIRCLE('',#104757,9.5);
#35098=CIRCLE('',#104759,9.5);
#35099=CIRCLE('',#104761,9.5);
#35100=CIRCLE('',#104763,9.5);
#35101=CIRCLE('',#104765,9.5);
#35102=CIRCLE('',#104767,9.5);
#35103=CIRCLE('',#104776,6.7);
#35104=CIRCLE('',#104778,6.7);
#43540=VERTEX_POINT('',#308949);
#43541=VERTEX_POINT('',#308950);
#43542=VERTEX_POINT('',#308952);
#43543=VERTEX_POINT('',#308961);
#43544=VERTEX_POINT('',#308978);
#43545=VERTEX_POINT('',#308979);
#43546=VERTEX_POINT('',#308981);
#43547=VERTEX_POINT('',#308998);
#43548=VERTEX_POINT('',#309021);
#43549=VERTEX_POINT('',#309022);
#43550=VERTEX_POINT('',#309097);
#43551=VERTEX_POINT('',#309098);
#43552=VERTEX_POINT('',#309173);
#43553=VERTEX_POINT('',#309174);
#43554=VERTEX_POINT('',#309249);
#43555=VERTEX_POINT('',#309250);
#43556=VERTEX_POINT('',#309252);
#43557=VERTEX_POINT('',#309271);
#43558=VERTEX_POINT('',#309273);
#43559=VERTEX_POINT('',#309298);
#43560=VERTEX_POINT('',#309299);
#43561=VERTEX_POINT('',#309330);
#43562=VERTEX_POINT('',#309331);
#43563=VERTEX_POINT('',#309376);
#43564=VERTEX_POINT('',#309377);
#43565=VERTEX_POINT('',#309422);
#43566=VERTEX_POINT('',#309423);
#43567=VERTEX_POINT('',#309425);
#43568=VERTEX_POINT('',#309767);
#43569=VERTEX_POINT('',#309819);
#43570=VERTEX_POINT('',#310211);
#43571=VERTEX_POINT('',#310212);
#43572=VERTEX_POINT('',#310223);
#43573=VERTEX_POINT('',#310225);
#43574=VERTEX_POINT('',#310238);
#43575=VERTEX_POINT('',#310239);
#43576=VERTEX_POINT('',#310250);
#43577=VERTEX_POINT('',#310252);
#43578=VERTEX_POINT('',#310265);
#43579=VERTEX_POINT('',#310266);
#43580=VERTEX_POINT('',#310277);
#43581=VERTEX_POINT('',#310279);
#43582=VERTEX_POINT('',#310292);
#43583=VERTEX_POINT('',#310293);
#43584=VERTEX_POINT('',#310304);
#43585=VERTEX_POINT('',#310306);
#43586=VERTEX_POINT('',#310319);
#43587=VERTEX_POINT('',#310320);
#43588=VERTEX_POINT('',#310331);
#43589=VERTEX_POINT('',#310333);
#43590=VERTEX_POINT('',#310346);
#43591=VERTEX_POINT('',#310347);
#43592=VERTEX_POINT('',#310358);
#43593=VERTEX_POINT('',#310360);
#43594=VERTEX_POINT('',#310373);
#43595=VERTEX_POINT('',#310377);
#43596=VERTEX_POINT('',#310386);
#43597=VERTEX_POINT('',#310395);
#43598=VERTEX_POINT('',#310404);
#43599=VERTEX_POINT('',#310413);
#43600=VERTEX_POINT('',#310427);
#43601=VERTEX_POINT('',#310431);
#43602=VERTEX_POINT('',#310440);
#43603=VERTEX_POINT('',#310449);
#43604=VERTEX_POINT('',#310458);
#43605=VERTEX_POINT('',#310467);
#43606=VERTEX_POINT('',#310488);
#43607=VERTEX_POINT('',#310491);
#57549=EDGE_CURVE('',#43540,#43541,#24804,.T.);
#57550=EDGE_CURVE('',#43542,#43540,#6898,.T.);
#57551=EDGE_CURVE('',#43543,#43542,#35085,.T.);
#57552=EDGE_CURVE('',#43541,#43543,#6899,.T.);
#57553=EDGE_CURVE('',#43544,#43545,#24805,.T.);
#57554=EDGE_CURVE('',#43546,#43545,#6900,.T.);
#57555=EDGE_CURVE('',#43546,#43547,#35086,.T.);
#57556=EDGE_CURVE('',#43544,#43547,#6901,.T.);
#57557=EDGE_CURVE('',#43548,#43549,#24806,.T.);
#57558=EDGE_CURVE('',#43545,#43549,#6902,.T.);
#57559=EDGE_CURVE('',#43548,#43544,#6903,.T.);
#57560=EDGE_CURVE('',#43550,#43551,#24807,.T.);
#57561=EDGE_CURVE('',#43549,#43551,#6904,.T.);
#57562=EDGE_CURVE('',#43550,#43548,#6905,.T.);
#57563=EDGE_CURVE('',#43552,#43553,#24808,.T.);
#57564=EDGE_CURVE('',#43551,#43553,#6906,.T.);
#57565=EDGE_CURVE('',#43552,#43550,#6907,.T.);
#57566=EDGE_CURVE('',#43554,#43555,#24809,.T.);
#57567=EDGE_CURVE('',#43556,#43554,#6908,.T.);
#57568=EDGE_CURVE('',#43556,#43557,#35087,.T.);
#57569=EDGE_CURVE('',#43557,#43558,#35088,.T.);
#57570=EDGE_CURVE('',#43555,#43558,#6909,.T.);
#57571=EDGE_CURVE('',#43559,#43560,#24810,.T.);
#57572=EDGE_CURVE('',#43560,#43543,#1738,.T.);
#57573=EDGE_CURVE('',#43559,#43542,#1739,.T.);
#57574=EDGE_CURVE('',#43561,#43562,#24811,.T.);
#57575=EDGE_CURVE('',#43562,#43560,#1740,.T.);
#57576=EDGE_CURVE('',#43561,#43559,#1741,.T.);
#57577=EDGE_CURVE('',#43563,#43564,#24812,.T.);
#57578=EDGE_CURVE('',#43564,#43562,#1742,.T.);
#57579=EDGE_CURVE('',#43563,#43561,#1743,.T.);
#57580=EDGE_CURVE('',#43565,#43566,#24813,.T.);
#57581=EDGE_CURVE('',#43565,#43567,#35089,.T.);
#57582=EDGE_CURVE('',#43567,#43566,#1744,.T.);
#57583=EDGE_CURVE('',#43553,#43555,#6910,.T.);
#57584=EDGE_CURVE('',#43558,#43541,#6911,.T.);
#57585=EDGE_CURVE('',#43566,#43564,#1745,.T.);
#57586=EDGE_CURVE('',#43567,#43568,#6912,.T.);
#57587=EDGE_CURVE('',#43568,#43546,#6913,.T.);
#57588=EDGE_CURVE('',#43569,#43563,#1746,.T.);
#57589=EDGE_CURVE('',#43569,#43565,#35090,.T.);
#57590=EDGE_CURVE('',#43540,#43556,#6914,.T.);
#57591=EDGE_CURVE('',#43554,#43552,#6915,.T.);
#57592=EDGE_CURVE('',#43547,#43569,#6916,.T.);
#57593=EDGE_CURVE('',#43570,#43571,#6917,.T.);
#57594=EDGE_CURVE('',#43572,#43570,#24814,.T.);
#57595=EDGE_CURVE('',#43573,#43572,#6918,.T.);
#57596=EDGE_CURVE('',#43571,#43573,#24815,.T.);
#57597=EDGE_CURVE('',#43574,#43575,#6919,.T.);
#57598=EDGE_CURVE('',#43576,#43574,#24816,.T.);
#57599=EDGE_CURVE('',#43577,#43576,#6920,.T.);
#57600=EDGE_CURVE('',#43575,#43577,#24817,.T.);
#57601=EDGE_CURVE('',#43578,#43579,#6921,.T.);
#57602=EDGE_CURVE('',#43580,#43578,#24818,.T.);
#57603=EDGE_CURVE('',#43581,#43580,#6922,.T.);
#57604=EDGE_CURVE('',#43579,#43581,#24819,.T.);
#57605=EDGE_CURVE('',#43582,#43583,#6923,.T.);
#57606=EDGE_CURVE('',#43584,#43582,#24820,.T.);
#57607=EDGE_CURVE('',#43585,#43584,#6924,.T.);
#57608=EDGE_CURVE('',#43583,#43585,#24821,.T.);
#57609=EDGE_CURVE('',#43586,#43587,#6925,.T.);
#57610=EDGE_CURVE('',#43588,#43586,#24822,.T.);
#57611=EDGE_CURVE('',#43589,#43588,#6926,.T.);
#57612=EDGE_CURVE('',#43587,#43589,#24823,.T.);
#57613=EDGE_CURVE('',#43590,#43591,#6927,.T.);
#57614=EDGE_CURVE('',#43592,#43590,#24824,.T.);
#57615=EDGE_CURVE('',#43593,#43592,#6928,.T.);
#57616=EDGE_CURVE('',#43591,#43593,#24825,.T.);
#57617=EDGE_CURVE('',#43593,#43594,#1747,.T.);
#57618=EDGE_CURVE('',#43595,#43592,#1748,.T.);
#57619=EDGE_CURVE('',#43594,#43595,#35091,.T.);
#57620=EDGE_CURVE('',#43589,#43595,#1749,.T.);
#57621=EDGE_CURVE('',#43596,#43588,#1750,.T.);
#57622=EDGE_CURVE('',#43595,#43596,#35092,.T.);
#57623=EDGE_CURVE('',#43585,#43596,#1751,.T.);
#57624=EDGE_CURVE('',#43597,#43584,#1752,.T.);
#57625=EDGE_CURVE('',#43596,#43597,#35093,.T.);
#57626=EDGE_CURVE('',#43581,#43597,#1753,.T.);
#57627=EDGE_CURVE('',#43598,#43580,#1754,.T.);
#57628=EDGE_CURVE('',#43597,#43598,#35094,.T.);
#57629=EDGE_CURVE('',#43577,#43598,#1755,.T.);
#57630=EDGE_CURVE('',#43599,#43576,#1756,.T.);
#57631=EDGE_CURVE('',#43598,#43599,#35095,.T.);
#57632=EDGE_CURVE('',#43573,#43599,#1757,.T.);
#57633=EDGE_CURVE('',#43594,#43572,#1758,.T.);
#57634=EDGE_CURVE('',#43594,#43599,#35096,.T.);
#57635=EDGE_CURVE('',#43600,#43574,#1759,.T.);
#57636=EDGE_CURVE('',#43575,#43601,#1760,.T.);
#57637=EDGE_CURVE('',#43600,#43601,#35097,.T.);
#57638=EDGE_CURVE('',#43601,#43578,#1761,.T.);
#57639=EDGE_CURVE('',#43579,#43602,#1762,.T.);
#57640=EDGE_CURVE('',#43601,#43602,#35098,.T.);
#57641=EDGE_CURVE('',#43602,#43582,#1763,.T.);
#57642=EDGE_CURVE('',#43583,#43603,#1764,.T.);
#57643=EDGE_CURVE('',#43602,#43603,#35099,.T.);
#57644=EDGE_CURVE('',#43603,#43586,#1765,.T.);
#57645=EDGE_CURVE('',#43587,#43604,#1766,.T.);
#57646=EDGE_CURVE('',#43603,#43604,#35100,.T.);
#57647=EDGE_CURVE('',#43604,#43590,#1767,.T.);
#57648=EDGE_CURVE('',#43591,#43605,#1768,.T.);
#57649=EDGE_CURVE('',#43604,#43605,#35101,.T.);
#57650=EDGE_CURVE('',#43605,#43570,#1769,.T.);
#57651=EDGE_CURVE('',#43571,#43600,#1770,.T.);
#57652=EDGE_CURVE('',#43605,#43600,#35102,.T.);
#57653=EDGE_CURVE('',#43606,#43606,#35103,.T.);
#57654=EDGE_CURVE('',#43607,#43607,#35104,.T.);
#57655=EDGE_CURVE('',#43568,#43607,#24826,.T.);
#57656=EDGE_CURVE('',#43557,#43606,#24827,.T.);
#85539=ORIENTED_EDGE('',*,*,#57549,.F.);
#85540=ORIENTED_EDGE('',*,*,#57550,.F.);
#85541=ORIENTED_EDGE('',*,*,#57551,.F.);
#85542=ORIENTED_EDGE('',*,*,#57552,.F.);
#85543=ORIENTED_EDGE('',*,*,#57553,.T.);
#85544=ORIENTED_EDGE('',*,*,#57554,.F.);
#85545=ORIENTED_EDGE('',*,*,#57555,.T.);
#85546=ORIENTED_EDGE('',*,*,#57556,.F.);
#85547=ORIENTED_EDGE('',*,*,#57557,.T.);
#85548=ORIENTED_EDGE('',*,*,#57558,.F.);
#85549=ORIENTED_EDGE('',*,*,#57553,.F.);
#85550=ORIENTED_EDGE('',*,*,#57559,.F.);
#85551=ORIENTED_EDGE('',*,*,#57560,.T.);
#85552=ORIENTED_EDGE('',*,*,#57561,.F.);
#85553=ORIENTED_EDGE('',*,*,#57557,.F.);
#85554=ORIENTED_EDGE('',*,*,#57562,.F.);
#85555=ORIENTED_EDGE('',*,*,#57563,.T.);
#85556=ORIENTED_EDGE('',*,*,#57564,.F.);
#85557=ORIENTED_EDGE('',*,*,#57560,.F.);
#85558=ORIENTED_EDGE('',*,*,#57565,.F.);
#85559=ORIENTED_EDGE('',*,*,#57566,.F.);
#85560=ORIENTED_EDGE('',*,*,#57567,.F.);
#85561=ORIENTED_EDGE('',*,*,#57568,.T.);
#85562=ORIENTED_EDGE('',*,*,#57569,.T.);
#85563=ORIENTED_EDGE('',*,*,#57570,.F.);
#85564=ORIENTED_EDGE('',*,*,#57571,.T.);
#85565=ORIENTED_EDGE('',*,*,#57572,.T.);
#85566=ORIENTED_EDGE('',*,*,#57551,.T.);
#85567=ORIENTED_EDGE('',*,*,#57573,.F.);
#85568=ORIENTED_EDGE('',*,*,#57574,.T.);
#85569=ORIENTED_EDGE('',*,*,#57575,.T.);
#85570=ORIENTED_EDGE('',*,*,#57571,.F.);
#85571=ORIENTED_EDGE('',*,*,#57576,.F.);
#85572=ORIENTED_EDGE('',*,*,#57577,.T.);
#85573=ORIENTED_EDGE('',*,*,#57578,.T.);
#85574=ORIENTED_EDGE('',*,*,#57574,.F.);
#85575=ORIENTED_EDGE('',*,*,#57579,.F.);
#85576=ORIENTED_EDGE('',*,*,#57580,.F.);
#85577=ORIENTED_EDGE('',*,*,#57581,.T.);
#85578=ORIENTED_EDGE('',*,*,#57582,.T.);
#85579=ORIENTED_EDGE('',*,*,#57554,.T.);
#85580=ORIENTED_EDGE('',*,*,#57558,.T.);
#85581=ORIENTED_EDGE('',*,*,#57561,.T.);
#85582=ORIENTED_EDGE('',*,*,#57564,.T.);
#85583=ORIENTED_EDGE('',*,*,#57583,.T.);
#85584=ORIENTED_EDGE('',*,*,#57570,.T.);
#85585=ORIENTED_EDGE('',*,*,#57584,.T.);
#85586=ORIENTED_EDGE('',*,*,#57552,.T.);
#85587=ORIENTED_EDGE('',*,*,#57572,.F.);
#85588=ORIENTED_EDGE('',*,*,#57575,.F.);
#85589=ORIENTED_EDGE('',*,*,#57578,.F.);
#85590=ORIENTED_EDGE('',*,*,#57585,.F.);
#85591=ORIENTED_EDGE('',*,*,#57582,.F.);
#85592=ORIENTED_EDGE('',*,*,#57586,.T.);
#85593=ORIENTED_EDGE('',*,*,#57587,.T.);
#85594=ORIENTED_EDGE('',*,*,#57580,.T.);
#85595=ORIENTED_EDGE('',*,*,#57585,.T.);
#85596=ORIENTED_EDGE('',*,*,#57577,.F.);
#85597=ORIENTED_EDGE('',*,*,#57588,.F.);
#85598=ORIENTED_EDGE('',*,*,#57589,.T.);
#85599=ORIENTED_EDGE('',*,*,#57588,.T.);
#85600=ORIENTED_EDGE('',*,*,#57579,.T.);
#85601=ORIENTED_EDGE('',*,*,#57576,.T.);
#85602=ORIENTED_EDGE('',*,*,#57573,.T.);
#85603=ORIENTED_EDGE('',*,*,#57550,.T.);
#85604=ORIENTED_EDGE('',*,*,#57590,.T.);
#85605=ORIENTED_EDGE('',*,*,#57567,.T.);
#85606=ORIENTED_EDGE('',*,*,#57591,.T.);
#85607=ORIENTED_EDGE('',*,*,#57565,.T.);
#85608=ORIENTED_EDGE('',*,*,#57562,.T.);
#85609=ORIENTED_EDGE('',*,*,#57559,.T.);
#85610=ORIENTED_EDGE('',*,*,#57556,.T.);
#85611=ORIENTED_EDGE('',*,*,#57592,.T.);
#85612=ORIENTED_EDGE('',*,*,#57593,.F.);
#85613=ORIENTED_EDGE('',*,*,#57594,.F.);
#85614=ORIENTED_EDGE('',*,*,#57595,.F.);
#85615=ORIENTED_EDGE('',*,*,#57596,.F.);
#85616=ORIENTED_EDGE('',*,*,#57597,.F.);
#85617=ORIENTED_EDGE('',*,*,#57598,.F.);
#85618=ORIENTED_EDGE('',*,*,#57599,.F.);
#85619=ORIENTED_EDGE('',*,*,#57600,.F.);
#85620=ORIENTED_EDGE('',*,*,#57601,.F.);
#85621=ORIENTED_EDGE('',*,*,#57602,.F.);
#85622=ORIENTED_EDGE('',*,*,#57603,.F.);
#85623=ORIENTED_EDGE('',*,*,#57604,.F.);
#85624=ORIENTED_EDGE('',*,*,#57605,.F.);
#85625=ORIENTED_EDGE('',*,*,#57606,.F.);
#85626=ORIENTED_EDGE('',*,*,#57607,.F.);
#85627=ORIENTED_EDGE('',*,*,#57608,.F.);
#85628=ORIENTED_EDGE('',*,*,#57609,.F.);
#85629=ORIENTED_EDGE('',*,*,#57610,.F.);
#85630=ORIENTED_EDGE('',*,*,#57611,.F.);
#85631=ORIENTED_EDGE('',*,*,#57612,.F.);
#85632=ORIENTED_EDGE('',*,*,#57613,.F.);
#85633=ORIENTED_EDGE('',*,*,#57614,.F.);
#85634=ORIENTED_EDGE('',*,*,#57615,.F.);
#85635=ORIENTED_EDGE('',*,*,#57616,.F.);
#85636=ORIENTED_EDGE('',*,*,#57617,.F.);
#85637=ORIENTED_EDGE('',*,*,#57615,.T.);
#85638=ORIENTED_EDGE('',*,*,#57618,.F.);
#85639=ORIENTED_EDGE('',*,*,#57619,.F.);
#85640=ORIENTED_EDGE('',*,*,#57620,.F.);
#85641=ORIENTED_EDGE('',*,*,#57611,.T.);
#85642=ORIENTED_EDGE('',*,*,#57621,.F.);
#85643=ORIENTED_EDGE('',*,*,#57622,.F.);
#85644=ORIENTED_EDGE('',*,*,#57623,.F.);
#85645=ORIENTED_EDGE('',*,*,#57607,.T.);
#85646=ORIENTED_EDGE('',*,*,#57624,.F.);
#85647=ORIENTED_EDGE('',*,*,#57625,.F.);
#85648=ORIENTED_EDGE('',*,*,#57626,.F.);
#85649=ORIENTED_EDGE('',*,*,#57603,.T.);
#85650=ORIENTED_EDGE('',*,*,#57627,.F.);
#85651=ORIENTED_EDGE('',*,*,#57628,.F.);
#85652=ORIENTED_EDGE('',*,*,#57629,.F.);
#85653=ORIENTED_EDGE('',*,*,#57599,.T.);
#85654=ORIENTED_EDGE('',*,*,#57630,.F.);
#85655=ORIENTED_EDGE('',*,*,#57631,.F.);
#85656=ORIENTED_EDGE('',*,*,#57632,.F.);
#85657=ORIENTED_EDGE('',*,*,#57595,.T.);
#85658=ORIENTED_EDGE('',*,*,#57633,.F.);
#85659=ORIENTED_EDGE('',*,*,#57634,.T.);
#85660=ORIENTED_EDGE('',*,*,#57635,.T.);
#85661=ORIENTED_EDGE('',*,*,#57597,.T.);
#85662=ORIENTED_EDGE('',*,*,#57636,.T.);
#85663=ORIENTED_EDGE('',*,*,#57637,.F.);
#85664=ORIENTED_EDGE('',*,*,#57638,.T.);
#85665=ORIENTED_EDGE('',*,*,#57601,.T.);
#85666=ORIENTED_EDGE('',*,*,#57639,.T.);
#85667=ORIENTED_EDGE('',*,*,#57640,.F.);
#85668=ORIENTED_EDGE('',*,*,#57641,.T.);
#85669=ORIENTED_EDGE('',*,*,#57605,.T.);
#85670=ORIENTED_EDGE('',*,*,#57642,.T.);
#85671=ORIENTED_EDGE('',*,*,#57643,.F.);
#85672=ORIENTED_EDGE('',*,*,#57644,.T.);
#85673=ORIENTED_EDGE('',*,*,#57609,.T.);
#85674=ORIENTED_EDGE('',*,*,#57645,.T.);
#85675=ORIENTED_EDGE('',*,*,#57646,.F.);
#85676=ORIENTED_EDGE('',*,*,#57647,.T.);
#85677=ORIENTED_EDGE('',*,*,#57613,.T.);
#85678=ORIENTED_EDGE('',*,*,#57648,.T.);
#85679=ORIENTED_EDGE('',*,*,#57649,.F.);
#85680=ORIENTED_EDGE('',*,*,#57650,.T.);
#85681=ORIENTED_EDGE('',*,*,#57593,.T.);
#85682=ORIENTED_EDGE('',*,*,#57651,.T.);
#85683=ORIENTED_EDGE('',*,*,#57652,.F.);
#85684=ORIENTED_EDGE('',*,*,#57566,.T.);
#85685=ORIENTED_EDGE('',*,*,#57583,.F.);
#85686=ORIENTED_EDGE('',*,*,#57563,.F.);
#85687=ORIENTED_EDGE('',*,*,#57591,.F.);
#85688=ORIENTED_EDGE('',*,*,#57648,.F.);
#85689=ORIENTED_EDGE('',*,*,#57616,.T.);
#85690=ORIENTED_EDGE('',*,*,#57617,.T.);
#85691=ORIENTED_EDGE('',*,*,#57633,.T.);
#85692=ORIENTED_EDGE('',*,*,#57594,.T.);
#85693=ORIENTED_EDGE('',*,*,#57650,.F.);
#85694=ORIENTED_EDGE('',*,*,#57618,.T.);
#85695=ORIENTED_EDGE('',*,*,#57614,.T.);
#85696=ORIENTED_EDGE('',*,*,#57647,.F.);
#85697=ORIENTED_EDGE('',*,*,#57645,.F.);
#85698=ORIENTED_EDGE('',*,*,#57612,.T.);
#85699=ORIENTED_EDGE('',*,*,#57620,.T.);
#85700=ORIENTED_EDGE('',*,*,#57621,.T.);
#85701=ORIENTED_EDGE('',*,*,#57610,.T.);
#85702=ORIENTED_EDGE('',*,*,#57644,.F.);
#85703=ORIENTED_EDGE('',*,*,#57642,.F.);
#85704=ORIENTED_EDGE('',*,*,#57608,.T.);
#85705=ORIENTED_EDGE('',*,*,#57623,.T.);
#85706=ORIENTED_EDGE('',*,*,#57624,.T.);
#85707=ORIENTED_EDGE('',*,*,#57606,.T.);
#85708=ORIENTED_EDGE('',*,*,#57641,.F.);
#85709=ORIENTED_EDGE('',*,*,#57639,.F.);
#85710=ORIENTED_EDGE('',*,*,#57604,.T.);
#85711=ORIENTED_EDGE('',*,*,#57626,.T.);
#85712=ORIENTED_EDGE('',*,*,#57627,.T.);
#85713=ORIENTED_EDGE('',*,*,#57602,.T.);
#85714=ORIENTED_EDGE('',*,*,#57638,.F.);
#85715=ORIENTED_EDGE('',*,*,#57636,.F.);
#85716=ORIENTED_EDGE('',*,*,#57600,.T.);
#85717=ORIENTED_EDGE('',*,*,#57629,.T.);
#85718=ORIENTED_EDGE('',*,*,#57630,.T.);
#85719=ORIENTED_EDGE('',*,*,#57598,.T.);
#85720=ORIENTED_EDGE('',*,*,#57635,.F.);
#85721=ORIENTED_EDGE('',*,*,#57651,.F.);
#85722=ORIENTED_EDGE('',*,*,#57596,.T.);
#85723=ORIENTED_EDGE('',*,*,#57632,.T.);
#85724=ORIENTED_EDGE('',*,*,#57649,.T.);
#85725=ORIENTED_EDGE('',*,*,#57652,.T.);
#85726=ORIENTED_EDGE('',*,*,#57637,.T.);
#85727=ORIENTED_EDGE('',*,*,#57640,.T.);
#85728=ORIENTED_EDGE('',*,*,#57643,.T.);
#85729=ORIENTED_EDGE('',*,*,#57646,.T.);
#85730=ORIENTED_EDGE('',*,*,#57653,.T.);
#85731=ORIENTED_EDGE('',*,*,#57634,.F.);
#85732=ORIENTED_EDGE('',*,*,#57619,.T.);
#85733=ORIENTED_EDGE('',*,*,#57622,.T.);
#85734=ORIENTED_EDGE('',*,*,#57625,.T.);
#85735=ORIENTED_EDGE('',*,*,#57628,.T.);
#85736=ORIENTED_EDGE('',*,*,#57631,.T.);
#85737=ORIENTED_EDGE('',*,*,#57654,.T.);
#85738=ORIENTED_EDGE('',*,*,#57586,.F.);
#85739=ORIENTED_EDGE('',*,*,#57581,.F.);
#85740=ORIENTED_EDGE('',*,*,#57589,.F.);
#85741=ORIENTED_EDGE('',*,*,#57592,.F.);
#85742=ORIENTED_EDGE('',*,*,#57555,.F.);
#85743=ORIENTED_EDGE('',*,*,#57587,.F.);
#85744=ORIENTED_EDGE('',*,*,#57655,.T.);
#85745=ORIENTED_EDGE('',*,*,#57654,.F.);
#85746=ORIENTED_EDGE('',*,*,#57655,.F.);
#85747=ORIENTED_EDGE('',*,*,#57549,.T.);
#85748=ORIENTED_EDGE('',*,*,#57584,.F.);
#85749=ORIENTED_EDGE('',*,*,#57569,.F.);
#85750=ORIENTED_EDGE('',*,*,#57656,.T.);
#85751=ORIENTED_EDGE('',*,*,#57653,.F.);
#85752=ORIENTED_EDGE('',*,*,#57656,.F.);
#85753=ORIENTED_EDGE('',*,*,#57568,.F.);
#85754=ORIENTED_EDGE('',*,*,#57590,.F.);
#87950=CYLINDRICAL_SURFACE('',#104723,6.);
#87951=CYLINDRICAL_SURFACE('',#104725,6.);
#87952=CYLINDRICAL_SURFACE('',#104726,6.);
#87953=CYLINDRICAL_SURFACE('',#104727,6.);
#87954=CYLINDRICAL_SURFACE('',#104728,6.);
#87955=CYLINDRICAL_SURFACE('',#104731,4.86334165753295);
#87956=CYLINDRICAL_SURFACE('',#104732,4.86334165753295);
#87957=CYLINDRICAL_SURFACE('',#104733,4.86334165753295);
#87958=CYLINDRICAL_SURFACE('',#104734,4.86334165753295);
#87959=CYLINDRICAL_SURFACE('',#104736,4.86334165753295);
#87960=CYLINDRICAL_SURFACE('',#104738,0.285000000000001);
#87961=CYLINDRICAL_SURFACE('',#104739,0.285);
#87962=CYLINDRICAL_SURFACE('',#104740,0.285000000000001);
#87963=CYLINDRICAL_SURFACE('',#104741,0.285000000000001);
#87964=CYLINDRICAL_SURFACE('',#104742,0.285);
#87965=CYLINDRICAL_SURFACE('',#104743,0.285000000000001);
#87966=CYLINDRICAL_SURFACE('',#104768,6.);
#93664=ADVANCED_FACE('',(#14385),#7207,.F.);
#93665=ADVANCED_FACE('',(#14386),#87950,.F.);
#93666=ADVANCED_FACE('',(#14387),#87951,.F.);
#93667=ADVANCED_FACE('',(#14388),#87952,.F.);
#93668=ADVANCED_FACE('',(#14389),#87953,.F.);
#93669=ADVANCED_FACE('',(#14390),#87954,.F.);
#93670=ADVANCED_FACE('',(#14391),#87955,.F.);
#93671=ADVANCED_FACE('',(#14392),#87956,.F.);
#93672=ADVANCED_FACE('',(#14393),#87957,.F.);
#93673=ADVANCED_FACE('',(#14394),#87958,.F.);
#93674=ADVANCED_FACE('',(#14395),#3204,.F.);
#93675=ADVANCED_FACE('',(#14396),#87959,.F.);
#93676=ADVANCED_FACE('',(#14397),#3205,.F.);
#93677=ADVANCED_FACE('',(#14398),#87960,.T.);
#93678=ADVANCED_FACE('',(#14399),#87961,.T.);
#93679=ADVANCED_FACE('',(#14400),#87962,.T.);
#93680=ADVANCED_FACE('',(#14401),#87963,.T.);
#93681=ADVANCED_FACE('',(#14402),#87964,.T.);
#93682=ADVANCED_FACE('',(#14403),#87965,.T.);
#93683=ADVANCED_FACE('',(#14404),#7208,.T.);
#93684=ADVANCED_FACE('',(#14405),#7209,.T.);
#93685=ADVANCED_FACE('',(#14406),#7210,.T.);
#93686=ADVANCED_FACE('',(#14407),#7211,.T.);
#93687=ADVANCED_FACE('',(#14408),#7212,.T.);
#93688=ADVANCED_FACE('',(#14409),#7213,.T.);
#93689=ADVANCED_FACE('',(#14410),#7214,.T.);
#93690=ADVANCED_FACE('',(#14411),#7215,.T.);
#93691=ADVANCED_FACE('',(#14412),#7216,.T.);
#93692=ADVANCED_FACE('',(#14413),#7217,.T.);
#93693=ADVANCED_FACE('',(#14414),#7218,.T.);
#93694=ADVANCED_FACE('',(#14415),#7219,.T.);
#93695=ADVANCED_FACE('',(#14416),#87966,.F.);
#93696=ADVANCED_FACE('',(#14417),#8680,.F.);
#93697=ADVANCED_FACE('',(#14418),#8681,.F.);
#93698=ADVANCED_FACE('',(#14419),#8682,.F.);
#93699=ADVANCED_FACE('',(#14420),#8683,.F.);
#93700=ADVANCED_FACE('',(#14421),#8684,.F.);
#93701=ADVANCED_FACE('',(#14422),#8685,.F.);
#93702=ADVANCED_FACE('',(#14423,#7704),#8686,.T.);
#93703=ADVANCED_FACE('',(#14424,#7705),#8687,.F.);
#93704=ADVANCED_FACE('',(#14425),#7220,.F.);
#93705=ADVANCED_FACE('',(#14426),#7221,.F.);
#93774=CLOSED_SHELL('',(#93664,#93665,#93666,#93667,#93668,#93669,#93670,
#93671,#93672,#93673,#93674,#93675,#93676,#93677,#93678,#93679,#93680,#93681,
#93682,#93683,#93684,#93685,#93686,#93687,#93688,#93689,#93690,#93691,#93692,
#93693,#93694,#93695,#93696,#93697,#93698,#93699,#93700,#93701,#93702,#93703,
#93704,#93705));
#104720=AXIS2_PLACEMENT_3D('',#308947,#130701,#130702);
#104721=AXIS2_PLACEMENT_3D('',#308948,#130703,#130704);
#104722=AXIS2_PLACEMENT_3D('',#308962,#130706,#130707);
#104723=AXIS2_PLACEMENT_3D('',#308977,#130708,#130709);
#104724=AXIS2_PLACEMENT_3D('',#308999,#130711,#130712);
#104725=AXIS2_PLACEMENT_3D('',#309020,#130713,#130714);
#104726=AXIS2_PLACEMENT_3D('',#309096,#130716,#130717);
#104727=AXIS2_PLACEMENT_3D('',#309172,#130719,#130720);
#104728=AXIS2_PLACEMENT_3D('',#309248,#130722,#130723);
#104729=AXIS2_PLACEMENT_3D('',#309272,#130725,#130726);
#104730=AXIS2_PLACEMENT_3D('',#309274,#130727,#130728);
#104731=AXIS2_PLACEMENT_3D('',#309297,#130729,#130730);
#104732=AXIS2_PLACEMENT_3D('',#309329,#130732,#130733);
#104733=AXIS2_PLACEMENT_3D('',#309375,#130735,#130736);
#104734=AXIS2_PLACEMENT_3D('',#309421,#130738,#130739);
#104735=AXIS2_PLACEMENT_3D('',#309426,#130741,#130742);
#104736=AXIS2_PLACEMENT_3D('',#309818,#130743,#130744);
#104737=AXIS2_PLACEMENT_3D('',#309841,#130745,#130746);
#104738=AXIS2_PLACEMENT_3D('',#310210,#130747,#130748);
#104739=AXIS2_PLACEMENT_3D('',#310237,#130751,#130752);
#104740=AXIS2_PLACEMENT_3D('',#310264,#130755,#130756);
#104741=AXIS2_PLACEMENT_3D('',#310291,#130759,#130760);
#104742=AXIS2_PLACEMENT_3D('',#310318,#130763,#130764);
#104743=AXIS2_PLACEMENT_3D('',#310345,#130767,#130768);
#104744=AXIS2_PLACEMENT_3D('',#310372,#130771,#130772);
#104745=AXIS2_PLACEMENT_3D('',#310381,#130773,#130774);
#104746=AXIS2_PLACEMENT_3D('',#310382,#130775,#130776);
#104747=AXIS2_PLACEMENT_3D('',#310390,#130777,#130778);
#104748=AXIS2_PLACEMENT_3D('',#310391,#130779,#130780);
#104749=AXIS2_PLACEMENT_3D('',#310399,#130781,#130782);
#104750=AXIS2_PLACEMENT_3D('',#310400,#130783,#130784);
#104751=AXIS2_PLACEMENT_3D('',#310408,#130785,#130786);
#104752=AXIS2_PLACEMENT_3D('',#310409,#130787,#130788);
#104753=AXIS2_PLACEMENT_3D('',#310417,#130789,#130790);
#104754=AXIS2_PLACEMENT_3D('',#310418,#130791,#130792);
#104755=AXIS2_PLACEMENT_3D('',#310425,#130793,#130794);
#104756=AXIS2_PLACEMENT_3D('',#310426,#130795,#130796);
#104757=AXIS2_PLACEMENT_3D('',#310435,#130797,#130798);
#104758=AXIS2_PLACEMENT_3D('',#310436,#130799,#130800);
#104759=AXIS2_PLACEMENT_3D('',#310444,#130801,#130802);
#104760=AXIS2_PLACEMENT_3D('',#310445,#130803,#130804);
#104761=AXIS2_PLACEMENT_3D('',#310453,#130805,#130806);
#104762=AXIS2_PLACEMENT_3D('',#310454,#130807,#130808);
#104763=AXIS2_PLACEMENT_3D('',#310462,#130809,#130810);
#104764=AXIS2_PLACEMENT_3D('',#310463,#130811,#130812);
#104765=AXIS2_PLACEMENT_3D('',#310471,#130813,#130814);
#104766=AXIS2_PLACEMENT_3D('',#310472,#130815,#130816);
#104767=AXIS2_PLACEMENT_3D('',#310479,#130817,#130818);
#104768=AXIS2_PLACEMENT_3D('',#310480,#130819,#130820);
#104769=AXIS2_PLACEMENT_3D('',#310481,#130821,#130822);
#104770=AXIS2_PLACEMENT_3D('',#310482,#130823,#130824);
#104771=AXIS2_PLACEMENT_3D('',#310483,#130825,#130826);
#104772=AXIS2_PLACEMENT_3D('',#310484,#130827,#130828);
#104773=AXIS2_PLACEMENT_3D('',#310485,#130829,#130830);
#104774=AXIS2_PLACEMENT_3D('',#310486,#130831,#130832);
#104775=AXIS2_PLACEMENT_3D('',#310487,#130833,#130834);
#104776=AXIS2_PLACEMENT_3D('',#310489,#130835,#130836);
#104777=AXIS2_PLACEMENT_3D('',#310490,#130837,#130838);
#104778=AXIS2_PLACEMENT_3D('',#310492,#130839,#130840);
#104779=AXIS2_PLACEMENT_3D('',#310493,#130841,#130842);
#104780=AXIS2_PLACEMENT_3D('',#310495,#130844,#130845);
#130701=DIRECTION('axis',(0.,0.,1.));
#130702=DIRECTION('refdir',(1.,0.,0.));
#130703=DIRECTION('center_axis',(0.,0.,1.));
#130704=DIRECTION('ref_axis',(1.,0.,0.));
#130705=DIRECTION('',(-0.70710678118655,-8.65956056235497E-17,0.707106781186545));
#130706=DIRECTION('center_axis',(0.,0.,1.));
#130707=DIRECTION('ref_axis',(-6.16388274026379E-15,1.,0.));
#130708=DIRECTION('center_axis',(0.,0.,-1.));
#130709=DIRECTION('ref_axis',(-1.,0.,0.));
#130710=DIRECTION('',(0.,0.,-1.));
#130711=DIRECTION('center_axis',(0.,0.,-1.));
#130712=DIRECTION('ref_axis',(1.,0.,0.));
#130713=DIRECTION('center_axis',(0.,0.,-1.));
#130714=DIRECTION('ref_axis',(-1.,0.,0.));
#130715=DIRECTION('',(0.,0.,-1.));
#130716=DIRECTION('center_axis',(0.,0.,-1.));
#130717=DIRECTION('ref_axis',(-1.,0.,0.));
#130718=DIRECTION('',(0.,0.,-1.));
#130719=DIRECTION('center_axis',(0.,0.,-1.));
#130720=DIRECTION('ref_axis',(-1.,0.,0.));
#130721=DIRECTION('',(0.,0.,-1.));
#130722=DIRECTION('center_axis',(0.,0.,-1.));
#130723=DIRECTION('ref_axis',(-1.,0.,0.));
#130724=DIRECTION('',(0.,0.,-1.));
#130725=DIRECTION('center_axis',(0.,0.,1.));
#130726=DIRECTION('ref_axis',(1.,0.,0.));
#130727=DIRECTION('center_axis',(0.,0.,1.));
#130728=DIRECTION('ref_axis',(1.,0.,0.));
#130729=DIRECTION('center_axis',(0.,0.,1.));
#130730=DIRECTION('ref_axis',(-6.16388274026379E-15,1.,0.));
#130731=DIRECTION('',(0.,0.,1.));
#130732=DIRECTION('center_axis',(0.,0.,1.));
#130733=DIRECTION('ref_axis',(-6.16388274026379E-15,1.,0.));
#130734=DIRECTION('',(0.,0.,1.));
#130735=DIRECTION('center_axis',(0.,0.,1.));
#130736=DIRECTION('ref_axis',(-6.16388274026379E-15,1.,0.));
#130737=DIRECTION('',(0.,0.,1.));
#130738=DIRECTION('center_axis',(0.,0.,1.));
#130739=DIRECTION('ref_axis',(-6.16388274026379E-15,1.,0.));
#130740=DIRECTION('',(0.,0.,1.));
#130741=DIRECTION('center_axis',(0.,0.,-1.));
#130742=DIRECTION('ref_axis',(-6.16388274026379E-15,1.,0.));
#130743=DIRECTION('center_axis',(0.,0.,1.));
#130744=DIRECTION('ref_axis',(-6.16388274026379E-15,1.,0.));
#130745=DIRECTION('center_axis',(0.,0.,-1.));
#130746=DIRECTION('ref_axis',(-6.16388274026379E-15,1.,0.));
#130747=DIRECTION('center_axis',(0.,0.,-1.));
#130748=DIRECTION('ref_axis',(-1.,0.,0.));
#130749=DIRECTION('',(0.,0.,1.));
#130750=DIRECTION('',(0.,0.,-1.));
#130751=DIRECTION('center_axis',(0.,0.,-1.));
#130752=DIRECTION('ref_axis',(-1.,0.,0.));
#130753=DIRECTION('',(0.,0.,1.));
#130754=DIRECTION('',(0.,0.,-1.));
#130755=DIRECTION('center_axis',(0.,0.,-1.));
#130756=DIRECTION('ref_axis',(-1.,0.,0.));
#130757=DIRECTION('',(0.,0.,1.));
#130758=DIRECTION('',(0.,0.,-1.));
#130759=DIRECTION('center_axis',(0.,0.,-1.));
#130760=DIRECTION('ref_axis',(-1.,0.,0.));
#130761=DIRECTION('',(0.,0.,1.));
#130762=DIRECTION('',(0.,0.,-1.));
#130763=DIRECTION('center_axis',(0.,0.,-1.));
#130764=DIRECTION('ref_axis',(-1.,0.,0.));
#130765=DIRECTION('',(0.,0.,1.));
#130766=DIRECTION('',(0.,0.,-1.));
#130767=DIRECTION('center_axis',(0.,0.,-1.));
#130768=DIRECTION('ref_axis',(-1.,0.,0.));
#130769=DIRECTION('',(0.,0.,1.));
#130770=DIRECTION('',(0.,0.,-1.));
#130771=DIRECTION('center_axis',(0.,0.,1.));
#130772=DIRECTION('ref_axis',(1.,0.,0.));
#130773=DIRECTION('center_axis',(0.,0.,-1.));
#130774=DIRECTION('ref_axis',(1.,0.,0.));
#130775=DIRECTION('center_axis',(0.,0.,1.));
#130776=DIRECTION('ref_axis',(1.,0.,0.));
#130777=DIRECTION('center_axis',(0.,0.,-1.));
#130778=DIRECTION('ref_axis',(1.,0.,0.));
#130779=DIRECTION('center_axis',(0.,0.,1.));
#130780=DIRECTION('ref_axis',(1.,0.,0.));
#130781=DIRECTION('center_axis',(0.,0.,-1.));
#130782=DIRECTION('ref_axis',(1.,1.77635683940025E-15,0.));
#130783=DIRECTION('center_axis',(0.,0.,1.));
#130784=DIRECTION('ref_axis',(1.,0.,0.));
#130785=DIRECTION('center_axis',(0.,0.,-1.));
#130786=DIRECTION('ref_axis',(1.,0.,0.));
#130787=DIRECTION('center_axis',(0.,0.,1.));
#130788=DIRECTION('ref_axis',(1.,0.,0.));
#130789=DIRECTION('center_axis',(0.,0.,-1.));
#130790=DIRECTION('ref_axis',(1.,1.77635683940025E-15,0.));
#130791=DIRECTION('center_axis',(0.,0.,1.));
#130792=DIRECTION('ref_axis',(1.,0.,0.));
#130793=DIRECTION('center_axis',(0.,0.,1.));
#130794=DIRECTION('ref_axis',(1.,0.,0.));
#130795=DIRECTION('center_axis',(0.,0.,-1.));
#130796=DIRECTION('ref_axis',(1.,0.,0.));
#130797=DIRECTION('center_axis',(0.,0.,1.));
#130798=DIRECTION('ref_axis',(1.,0.,0.));
#130799=DIRECTION('center_axis',(0.,0.,-1.));
#130800=DIRECTION('ref_axis',(1.,0.,0.));
#130801=DIRECTION('center_axis',(0.,0.,1.));
#130802=DIRECTION('ref_axis',(1.,0.,0.));
#130803=DIRECTION('center_axis',(0.,0.,-1.));
#130804=DIRECTION('ref_axis',(1.,0.,0.));
#130805=DIRECTION('center_axis',(0.,0.,1.));
#130806=DIRECTION('ref_axis',(1.,0.,0.));
#130807=DIRECTION('center_axis',(0.,0.,-1.));
#130808=DIRECTION('ref_axis',(1.,0.,0.));
#130809=DIRECTION('center_axis',(0.,0.,1.));
#130810=DIRECTION('ref_axis',(1.,0.,0.));
#130811=DIRECTION('center_axis',(0.,0.,-1.));
#130812=DIRECTION('ref_axis',(1.,0.,0.));
#130813=DIRECTION('center_axis',(0.,0.,1.));
#130814=DIRECTION('ref_axis',(1.,0.,0.));
#130815=DIRECTION('center_axis',(0.,0.,-1.));
#130816=DIRECTION('ref_axis',(1.,0.,0.));
#130817=DIRECTION('center_axis',(0.,0.,1.));
#130818=DIRECTION('ref_axis',(1.,0.,0.));
#130819=DIRECTION('center_axis',(0.,0.,-1.));
#130820=DIRECTION('ref_axis',(-1.,0.,0.));
#130821=DIRECTION('center_axis',(-1.,0.,0.));
#130822=DIRECTION('ref_axis',(0.,0.,1.));
#130823=DIRECTION('center_axis',(-0.5,0.866025403784439,0.));
#130824=DIRECTION('ref_axis',(0.,0.,1.));
#130825=DIRECTION('center_axis',(0.5,0.866025403784439,0.));
#130826=DIRECTION('ref_axis',(0.,0.,-1.));
#130827=DIRECTION('center_axis',(1.,0.,0.));
#130828=DIRECTION('ref_axis',(0.,1.,0.));
#130829=DIRECTION('center_axis',(0.5,-0.866025403784439,0.));
#130830=DIRECTION('ref_axis',(0.,0.,-1.));
#130831=DIRECTION('center_axis',(-0.5,-0.866025403784439,0.));
#130832=DIRECTION('ref_axis',(-0.866025403784439,0.5,0.));
#130833=DIRECTION('center_axis',(0.,0.,1.));
#130834=DIRECTION('ref_axis',(1.,0.,0.));
#130835=DIRECTION('center_axis',(0.,0.,-1.));
#130836=DIRECTION('ref_axis',(1.,0.,0.));
#130837=DIRECTION('center_axis',(0.,0.,1.));
#130838=DIRECTION('ref_axis',(1.,0.,0.));
#130839=DIRECTION('center_axis',(0.,0.,1.));
#130840=DIRECTION('ref_axis',(1.,0.,0.));
#130841=DIRECTION('center_axis',(0.,0.,-1.));
#130842=DIRECTION('ref_axis',(-1.,0.,0.));
#130843=DIRECTION('',(0.707106781186547,-8.65956056235493E-17,-0.707106781186548));
#130844=DIRECTION('center_axis',(0.,0.,1.));
#130845=DIRECTION('ref_axis',(1.,0.,0.));
#130846=DIRECTION('',(-0.70710678118655,-8.65956056235497E-17,0.707106781186545));
#308947=CARTESIAN_POINT('',(0.,0.,0.));
#308948=CARTESIAN_POINT('Origin',(0.,8.67361737988403E-16,4.3));
#308949=CARTESIAN_POINT('',(-4.95790425747066,1.64791259544213E-16,3.25790425747067));
#308950=CARTESIAN_POINT('',(-5.73382214207426,-3.69911165529381E-15,4.03382214207426));
#308951=CARTESIAN_POINT('',(-6.,1.32573658499991E-16,4.3));
#308952=CARTESIAN_POINT('',(-4.17899100816595,2.48759446686254,3.1633416575335));
#308953=CARTESIAN_POINT('Ctrl Pts',(-4.17899100816605,2.48759446686292,
3.1633416575334));
#308954=CARTESIAN_POINT('Ctrl Pts',(-4.35976599882962,2.2078253190039,3.1755770463795));
#308955=CARTESIAN_POINT('Ctrl Pts',(-4.51120120864995,1.9101569924174,3.18761785547117));
#308956=CARTESIAN_POINT('Ctrl Pts',(-4.75167253802496,1.28565862670522,
3.21105851922133));
#308957=CARTESIAN_POINT('Ctrl Pts',(-4.84071390792199,0.958207282422365,
3.2229942327288));
#308958=CARTESIAN_POINT('Ctrl Pts',(-4.9296140215725,0.416876072737902,
3.24277553752449));
#308959=CARTESIAN_POINT('Ctrl Pts',(-4.95035223594235,0.208575748336291,
3.25035223594236));
#308960=CARTESIAN_POINT('Ctrl Pts',(-4.95790425747066,-1.0998146837693E-14,
3.25790425747067));
#308961=CARTESIAN_POINT('',(-1.20731623616734,4.71110173778723,3.16334165753294));
#308962=CARTESIAN_POINT('Origin',(2.99770677028732E-14,-1.99840144432528E-14,
3.16334165753296));
#308963=CARTESIAN_POINT('Ctrl Pts',(-5.73382214207426,-1.47104550762833E-14,
4.03382214207426));
#308964=CARTESIAN_POINT('Ctrl Pts',(-5.67965864914995,0.463559823425577,
3.97965864914995));
#308965=CARTESIAN_POINT('Ctrl Pts',(-5.56866706255198,0.919207299152243,
3.92486143298303));
#308966=CARTESIAN_POINT('Ctrl Pts',(-5.34205662154187,1.51737050224436,
3.85075284488971));
#308967=CARTESIAN_POINT('Ctrl Pts',(-5.2725514384,1.67890370382941,3.83071749499014));
#308968=CARTESIAN_POINT('Ctrl Pts',(-5.04000190306274,2.15372430153968,
3.76951790508672));
#308969=CARTESIAN_POINT('Ctrl Pts',(-4.85211037594447,2.4560892862115,3.72690108827535));
#308970=CARTESIAN_POINT('Ctrl Pts',(-4.21965696989943,3.27662074140819,
3.59952510479816));
#308971=CARTESIAN_POINT('Ctrl Pts',(-3.7037171783334,3.73029790186619,3.51307468723862));
#308972=CARTESIAN_POINT('Ctrl Pts',(-2.90020595016428,4.19934957757759,
3.39749471643447));
#308973=CARTESIAN_POINT('Ctrl Pts',(-2.5831446231689,4.36452052269484,3.35326171353216));
#308974=CARTESIAN_POINT('Ctrl Pts',(-1.85663861005444,4.60294910828577,
3.2525436348559));
#308975=CARTESIAN_POINT('Ctrl Pts',(-1.53427994520919,4.6735834616892,3.20816601785766));
#308976=CARTESIAN_POINT('Ctrl Pts',(-1.20731623616735,4.71110173778724,
3.16334165753295));
#308977=CARTESIAN_POINT('Origin',(0.,8.67361737988403E-16,5.));
#308978=CARTESIAN_POINT('',(6.,2.75510821701405E-15,-3.46875));
#308979=CARTESIAN_POINT('',(6.,2.98062226889103E-15,-3.6875));
#308980=CARTESIAN_POINT('',(6.,1.32573658499991E-16,5.));
#308981=CARTESIAN_POINT('',(-3.52671151375444,-4.85410196624999,-4.3));
#308982=CARTESIAN_POINT('Ctrl Pts',(-3.52671151375468,-4.8541019662498,
-4.29999999999999));
#308983=CARTESIAN_POINT('Ctrl Pts',(-3.01702740994254,-5.22440914351759,
-4.27172359402267));
#308984=CARTESIAN_POINT('Ctrl Pts',(-2.45213658317982,-5.51217749530336,
-4.24217304225748));
#308985=CARTESIAN_POINT('Ctrl Pts',(-1.25347469899042,-5.90134277786329,
-4.18269831181752));
#308986=CARTESIAN_POINT('Ctrl Pts',(-0.627290301592286,-6.00028203988638,
-4.1531587114977));
#308987=CARTESIAN_POINT('Ctrl Pts',(0.780649576506183,-5.9996503626714,
-4.08995709601937));
#308988=CARTESIAN_POINT('Ctrl Pts',(1.55112467953324,-5.84800091941097,
-4.05316439625781));
#308989=CARTESIAN_POINT('Ctrl Pts',(2.99115560746716,-5.25909995323094,
-3.9799435147521));
#308990=CARTESIAN_POINT('Ctrl Pts',(3.64708340346823,-4.82741575923643,
-3.94564211591625));
#308991=CARTESIAN_POINT('Ctrl Pts',(4.76587129969454,-3.72958885758529,
-3.87269323203537));
#308992=CARTESIAN_POINT('Ctrl Pts',(5.21476518269572,-3.07076816043726,
-3.83508774624553));
#308993=CARTESIAN_POINT('Ctrl Pts',(5.8254457701165,-1.63178380133655,-3.76320804987384));
#308994=CARTESIAN_POINT('Ctrl Pts',(5.98710430498857,-0.86783042733205,
-3.72845522456362));
#308995=CARTESIAN_POINT('Ctrl Pts',(5.99975331957655,-0.0628355432998811,
-3.69046537630555));
#308996=CARTESIAN_POINT('Ctrl Pts',(6.,-0.0314121545073137,-3.68898242306487));
#308997=CARTESIAN_POINT('Ctrl Pts',(6.,6.93787513263274E-15,-3.6875));
#308998=CARTESIAN_POINT('',(-5.92794875776502,-0.927050983124574,-4.3));
#308999=CARTESIAN_POINT('Origin',(0.,8.67361737988403E-16,-4.3));
#309000=CARTESIAN_POINT('Ctrl Pts',(6.,2.0122792321331E-15,-3.46875));
#309001=CARTESIAN_POINT('Ctrl Pts',(6.,-0.292663539025992,-3.48256157030785));
#309002=CARTESIAN_POINT('Ctrl Pts',(5.97858754364113,-0.585590117231843,
-3.49638555413373));
#309003=CARTESIAN_POINT('Ctrl Pts',(5.82222002909116,-1.64460792499764,
-3.54636341935705));
#309004=CARTESIAN_POINT('Ctrl Pts',(5.5607466448591,-2.38349895084104,-3.58050080876941));
#309005=CARTESIAN_POINT('Ctrl Pts',(4.76927675868354,-3.72310608228378,
-3.65360125733108));
#309006=CARTESIAN_POINT('Ctrl Pts',(4.24579242054897,-4.31055256457267,
-3.69055077540168));
#309007=CARTESIAN_POINT('Ctrl Pts',(2.99271814667052,-5.26045286831389,
-3.76157686148056));
#309008=CARTESIAN_POINT('Ctrl Pts',(2.27204555389018,-5.60952042043114,
-3.79857954700951));
#309009=CARTESIAN_POINT('Ctrl Pts',(0.755636327633439,-6.00226359092732,
-3.87236787236862));
#309010=CARTESIAN_POINT('Ctrl Pts',(-0.0235323394529939,-6.04959639713139,
-3.90658291849198));
#309011=CARTESIAN_POINT('Ctrl Pts',(-1.56944643722608,-5.84420783515746,
-3.97896325289623));
#309012=CARTESIAN_POINT('Ctrl Pts',(-2.32079973347914,-5.58854451710374,
-4.01641457981235));
#309013=CARTESIAN_POINT('Ctrl Pts',(-3.67844415256058,-4.80419770598322,
-4.08878796902789));
#309014=CARTESIAN_POINT('Ctrl Pts',(-4.27248937251792,-4.28451816332565,
-4.12368375995929));
#309015=CARTESIAN_POINT('Ctrl Pts',(-5.05912931149185,-3.26512372236398,
-4.18442461750057));
#309016=CARTESIAN_POINT('Ctrl Pts',(-5.31626731416515,-2.82721615051172,
-4.2082765699416));
#309017=CARTESIAN_POINT('Ctrl Pts',(-5.71215595317702,-1.9028913933687,
-4.2545485907623));
#309018=CARTESIAN_POINT('Ctrl Pts',(-5.85073664177685,-1.42077729957134,
-4.27669974279977));
#309019=CARTESIAN_POINT('Ctrl Pts',(-5.92794875776501,-0.927050983124573,
-4.30000000000001));
#309020=CARTESIAN_POINT('Origin',(0.,8.67361737988403E-16,5.));
#309021=CARTESIAN_POINT('',(6.,3.32323015539645E-15,-1.71875));
#309022=CARTESIAN_POINT('',(6.,-5.58213622101655E-16,-1.9375));
#309023=CARTESIAN_POINT('',(6.,1.32573658499991E-16,5.));
#309024=CARTESIAN_POINT('Ctrl Pts',(6.,6.52256026967279E-15,-3.6875));
#309025=CARTESIAN_POINT('Ctrl Pts',(6.,0.754851426978661,-3.65187655476185));
#309026=CARTESIAN_POINT('Ctrl Pts',(5.85754231131096,1.50326411623468,-3.61758911902599));
#309027=CARTESIAN_POINT('Ctrl Pts',(5.29207719224363,2.93370952013802,-3.54728967566669));
#309028=CARTESIAN_POINT('Ctrl Pts',(4.86462320380596,3.59834926176515,-3.51005674514032));
#309029=CARTESIAN_POINT('Ctrl Pts',(3.78446274319373,4.71990668353304,-3.43727333018283));
#309030=CARTESIAN_POINT('Ctrl Pts',(3.14436250545196,5.16842862379681,-3.40325514303962));
#309031=CARTESIAN_POINT('Ctrl Pts',(1.71060281984634,5.80561894256311,-3.32961151325641));
#309032=CARTESIAN_POINT('Ctrl Pts',(0.927540309668796,5.98089784650727,
-3.29190925804666));
#309033=CARTESIAN_POINT('Ctrl Pts',(-0.642997127075086,6.01574222164111,
-3.22091085987786));
#309034=CARTESIAN_POINT('Ctrl Pts',(-1.41515883852677,5.88218433805444,
-3.18476544364091));
#309035=CARTESIAN_POINT('Ctrl Pts',(-2.86894581371622,5.32702879267005,
-3.11141927176926));
#309036=CARTESIAN_POINT('Ctrl Pts',(-3.53625863096382,4.90947819517605,
-3.07684941682089));
#309037=CARTESIAN_POINT('Ctrl Pts',(-4.6795110472583,3.83701775744516,-3.00419039101464));
#309038=CARTESIAN_POINT('Ctrl Pts',(-5.14230996632516,3.19016997761122,
-2.9666563133062));
#309039=CARTESIAN_POINT('Ctrl Pts',(-5.78559661601467,1.76775945417096,
-2.89450493598388));
#309040=CARTESIAN_POINT('Ctrl Pts',(-5.9650504210191,1.00810019736398,-2.8600749278492));
#309041=CARTESIAN_POINT('Ctrl Pts',(-6.02636626662587,-0.554006862010353,
-2.78635494362863));
#309042=CARTESIAN_POINT('Ctrl Pts',(-5.90116044522712,-1.34171831741748,
-2.74996681296589));
#309043=CARTESIAN_POINT('Ctrl Pts',(-5.3559200560131,-2.81498908441548,
-2.67859332848681));
#309044=CARTESIAN_POINT('Ctrl Pts',(-4.94440107418828,-3.48752970239708,
-2.64150076868213));
#309045=CARTESIAN_POINT('Ctrl Pts',(-3.89066652120622,-4.63291440095925,
-2.56854066851539));
#309046=CARTESIAN_POINT('Ctrl Pts',(-3.26006452534031,-5.09638730462185,
-2.53449878605424));
#309047=CARTESIAN_POINT('Ctrl Pts',(-1.84167979261482,-5.76512768826473,
-2.46108512339898));
#309048=CARTESIAN_POINT('Ctrl Pts',(-1.0646476216952,-5.95777476296554,
-2.42340024138862));
#309049=CARTESIAN_POINT('Ctrl Pts',(0.501567117423101,-6.02902034618537,
-2.35206500740862));
#309050=CARTESIAN_POINT('Ctrl Pts',(1.27536280312196,-5.91389860142432,
-2.316502392684));
#309051=CARTESIAN_POINT('Ctrl Pts',(2.74290332138521,-5.39333740010627,
-2.24304342297233));
#309052=CARTESIAN_POINT('Ctrl Pts',(3.42177892466692,-4.99029458024765,
-2.20811052867497));
#309053=CARTESIAN_POINT('Ctrl Pts',(4.58950176879661,-3.94387559037259,
-2.13576696772565));
#309054=CARTESIAN_POINT('Ctrl Pts',(5.066083143584,-3.30945112192263,-2.09832489426651));
#309055=CARTESIAN_POINT('Ctrl Pts',(5.74212308881292,-1.90426481076331,
-2.02592258302779));
#309056=CARTESIAN_POINT('Ctrl Pts',(5.93952523631834,-1.14901086376142,
-1.99172487673777));
#309057=CARTESIAN_POINT('Ctrl Pts',(5.99605415847058,-0.251399423361188,
-1.9493642070094));
#309058=CARTESIAN_POINT('Ctrl Pts',(6.,-0.125632992952679,-1.94342895487058));
#309059=CARTESIAN_POINT('Ctrl Pts',(6.,1.21430643318376E-15,-1.9375));
#309060=CARTESIAN_POINT('Ctrl Pts',(6.,8.2572837456496E-15,-1.71875));
#309061=CARTESIAN_POINT('Ctrl Pts',(6.,-0.380626147463122,-1.73671275960507));
#309062=CARTESIAN_POINT('Ctrl Pts',(5.96378105869915,-0.761301949215604,
-1.75467786252801));
#309063=CARTESIAN_POINT('Ctrl Pts',(5.74354061198417,-1.90264867938727,
-1.80854104843037));
#309064=CARTESIAN_POINT('Ctrl Pts',(5.44784922568642,-2.63234772832579,
-1.84313344932999));
#309065=CARTESIAN_POINT('Ctrl Pts',(4.59581412479552,-3.93460285458722,
-1.91648783842465));
#309066=CARTESIAN_POINT('Ctrl Pts',(4.04877122369217,-4.49554195946292,
-1.95258945402002));
#309067=CARTESIAN_POINT('Ctrl Pts',(2.75643213309168,-5.38826013945762,
-2.02361216748895));
#309068=CARTESIAN_POINT('Ctrl Pts',(2.01950923078473,-5.70550197669431,
-2.06131383676569));
#309069=CARTESIAN_POINT('Ctrl Pts',(0.484600928023682,-6.03033344932268,
-2.13494207511938));
#309070=CARTESIAN_POINT('Ctrl Pts',(-0.296964896493759,-6.04248112405295,
-2.1689591248813));
#309071=CARTESIAN_POINT('Ctrl Pts',(-1.82956974936608,-5.76759580806508,
-2.24175559630771));
#309072=CARTESIAN_POINT('Ctrl Pts',(-2.5654889922958,-5.48003748619595,
-2.27897933385702));
#309073=CARTESIAN_POINT('Ctrl Pts',(-3.8890650541548,-4.63622423181947,
-2.35069085588018));
#309074=CARTESIAN_POINT('Ctrl Pts',(-4.46303185697885,-4.08666189475346,
-2.38652333173586));
#309075=CARTESIAN_POINT('Ctrl Pts',(-5.35834192021326,-2.8083216078333,
-2.46016507094176));
#309076=CARTESIAN_POINT('Ctrl Pts',(-5.67542561455437,-2.09476336347253,
-2.49489254898579));
#309077=CARTESIAN_POINT('Ctrl Pts',(-6.0246894528286,-0.57123686740069,
-2.56679181387678));
#309078=CARTESIAN_POINT('Ctrl Pts',(-6.04750405750468,0.22552194160929,
-2.60439297986302));
#309079=CARTESIAN_POINT('Ctrl Pts',(-5.78526874443865,1.77087908084594,
-2.67732249083092));
#309080=CARTESIAN_POINT('Ctrl Pts',(-5.50714127525806,2.50533946687444,
-2.71163960583237));
#309081=CARTESIAN_POINT('Ctrl Pts',(-4.68608114771929,3.82697580146689,
-2.78487474353452));
#309082=CARTESIAN_POINT('Ctrl Pts',(-4.15102714321106,4.40156948651998,
-2.82162948145506));
#309083=CARTESIAN_POINT('Ctrl Pts',(-2.8765788559961,5.32535707165584,-2.89230229954621));
#309084=CARTESIAN_POINT('Ctrl Pts',(-2.14521668281624,5.65968734390764,
-2.93000359360147));
#309085=CARTESIAN_POINT('Ctrl Pts',(-0.616665035412588,6.01817695082359,
-3.00383737471598));
#309086=CARTESIAN_POINT('Ctrl Pts',(0.163766668494401,6.04747253546172,
-3.03790801272646));
#309087=CARTESIAN_POINT('Ctrl Pts',(1.70309619005384,5.80642697848102,-3.11051281019814));
#309088=CARTESIAN_POINT('Ctrl Pts',(2.44671138181905,5.53432659170943,-3.14785653591319));
#309089=CARTESIAN_POINT('Ctrl Pts',(3.7871031240861,4.71943158303236,-3.21990106976846));
#309090=CARTESIAN_POINT('Ctrl Pts',(4.37095580452145,4.18448897586484,-3.25523421552925));
#309091=CARTESIAN_POINT('Ctrl Pts',(5.29372927427807,2.9284545028034,-3.32878613780276));
#309092=CARTESIAN_POINT('Ctrl Pts',(5.62704057338196,2.22166316356583,-3.36390381011906));
#309093=CARTESIAN_POINT('Ctrl Pts',(5.93875916593771,0.989102212585849,
-3.42207163754923));
#309094=CARTESIAN_POINT('Ctrl Pts',(6.,0.494927234506341,-3.44539306828448));
#309095=CARTESIAN_POINT('Ctrl Pts',(6.,1.11022302462516E-15,-3.46875));
#309096=CARTESIAN_POINT('Origin',(0.,8.67361737988403E-16,5.));
#309097=CARTESIAN_POINT('',(6.,8.4276539834582E-15,0.0312499999999995));
#309098=CARTESIAN_POINT('',(6.,-1.04393619537516E-15,-0.187499999999998));
#309099=CARTESIAN_POINT('',(6.,1.32573658499991E-16,5.));
#309100=CARTESIAN_POINT('Ctrl Pts',(6.,-9.71445146547012E-16,-1.9375));
#309101=CARTESIAN_POINT('Ctrl Pts',(6.,0.665640471875957,-1.90608665685633));
#309102=CARTESIAN_POINT('Ctrl Pts',(5.88921848914381,1.32755052273931,-1.87517647489086));
#309103=CARTESIAN_POINT('Ctrl Pts',(5.41705865771732,2.69496750715489,-1.80987164452479));
#309104=CARTESIAN_POINT('Ctrl Pts',(5.02159721538787,3.37503138930331,-1.77293727150543));
#309105=CARTESIAN_POINT('Ctrl Pts',(3.99457896445447,4.54384315513085,-1.69982382128799));
#309106=CARTESIAN_POINT('Ctrl Pts',(3.37352355036687,5.02220291135671,-1.66567301015243));
#309107=CARTESIAN_POINT('Ctrl Pts',(1.97078370548772,5.72203206182956,-1.59250815734831));
#309108=CARTESIAN_POINT('Ctrl Pts',(1.20010096420365,5.93173216826455,-1.55485956601145));
#309109=CARTESIAN_POINT('Ctrl Pts',(-0.361353151303249,6.0389314328722,
-1.4832136780329));
#309110=CARTESIAN_POINT('Ctrl Pts',(-1.13668683587222,5.94199046393976,
-1.44813624315785));
#309111=CARTESIAN_POINT('Ctrl Pts',(-2.61760268257367,5.45561539145597,
-1.37457549783133));
#309112=CARTESIAN_POINT('Ctrl Pts',(-3.30780631183448,5.06694972231676,
-1.33919869933545));
#309113=CARTESIAN_POINT('Ctrl Pts',(-4.49913774577299,4.04631668711824,
-1.26718475525266));
#309114=CARTESIAN_POINT('Ctrl Pts',(-4.98888502519728,3.42431115051731,
-1.22985162143565));
#309115=CARTESIAN_POINT('Ctrl Pts',(-5.69666279625056,2.03638239701799,
-1.15722781766094));
#309116=CARTESIAN_POINT('Ctrl Pts',(-5.91154129727581,1.28549067240917,
-1.12316572167189));
#309117=CARTESIAN_POINT('Ctrl Pts',(-6.04616476158962,-0.278633634974818,
-1.04935053815589));
#309118=CARTESIAN_POINT('Ctrl Pts',(-5.95590352725045,-1.07753162344421,
-1.011648418605));
#309119=CARTESIAN_POINT('Ctrl Pts',(-5.4744757179434,-2.57579237792346,
-0.940941511216246));
#309120=CARTESIAN_POINT('Ctrl Pts',(-5.09492912060133,-3.26290322787857,
-0.904252451447548));
#309121=CARTESIAN_POINT('Ctrl Pts',(-4.09435342234445,-4.45442056860119,
-0.831005603940027));
#309122=CARTESIAN_POINT('Ctrl Pts',(-3.48272795096895,-4.94734424768627,
-0.796666107542287));
#309123=CARTESIAN_POINT('Ctrl Pts',(-2.09560774824645,-5.67726362426316,
-0.723763493542176));
#309124=CARTESIAN_POINT('Ctrl Pts',(-1.33145851154505,-5.90340064515452,
-0.686168439737121));
#309125=CARTESIAN_POINT('Ctrl Pts',(0.224904569146673,-6.04548147749041,
-0.614242362558919));
#309126=CARTESIAN_POINT('Ctrl Pts',(1.00166095459279,-5.96616377216184,
-0.579549121659716));
#309127=CARTESIAN_POINT('Ctrl Pts',(2.49535830087068,-5.51299323361295,
-0.505898938545184));
#309128=CARTESIAN_POINT('Ctrl Pts',(3.19646467145431,-5.13833237345376,
-0.470012587137202));
#309129=CARTESIAN_POINT('Ctrl Pts',(4.41018090931122,-4.14277565323689,
-0.398335112895427));
#309130=CARTESIAN_POINT('Ctrl Pts',(4.91228199444614,-3.53294658077878,
-0.361124188318027));
#309131=CARTESIAN_POINT('Ctrl Pts',(5.65028338940432,-2.16198759426555,
-0.288309906928332));
#309132=CARTESIAN_POINT('Ctrl Pts',(5.88189550365007,-1.41534172658309,
-0.25429373806313));
#309133=CARTESIAN_POINT('Ctrl Pts',(5.98842683025393,-0.430575243748781,
-0.207819990223741));
#309134=CARTESIAN_POINT('Ctrl Pts',(6.,-0.215160329695893,-0.197653987855623));
#309135=CARTESIAN_POINT('Ctrl Pts',(6.,-5.34294830600857E-15,-0.187499999999998));
#309136=CARTESIAN_POINT('Ctrl Pts',(6.,3.19189119579733E-15,0.031249999999999));
#309137=CARTESIAN_POINT('Ctrl Pts',(6.,-0.470725023537795,0.00903523494968755));
#309138=CARTESIAN_POINT('Ctrl Pts',(5.94460269534144,-0.940908633524372,
-0.0131539793560597));
#309139=CARTESIAN_POINT('Ctrl Pts',(5.6510038405261,-2.16379476967363,-0.0708652265586574));
#309140=CARTESIAN_POINT('Ctrl Pts',(5.31985538512461,-2.88357663845083,
-0.106275724424197));
#309141=CARTESIAN_POINT('Ctrl Pts',(4.4055256383186,-4.14615152032113,-0.17984313561366));
#309142=CARTESIAN_POINT('Ctrl Pts',(3.83442737751384,-4.67935459625399,
-0.214890425153952));
#309143=CARTESIAN_POINT('Ctrl Pts',(2.50699655821698,-5.50821748300203,
-0.28655693361699));
#309144=CARTESIAN_POINT('Ctrl Pts',(1.75991933057626,-5.79034779941002,
-0.324202315297019));
#309145=CARTESIAN_POINT('Ctrl Pts',(0.213357498858581,-6.04630617784676,
-0.397349198359447));
#309146=CARTESIAN_POINT('Ctrl Pts',(-0.570328131021847,-6.02312656494286,
-0.431510709464236));
#309147=CARTESIAN_POINT('Ctrl Pts',(-2.08765133392454,-5.67880280627236,
-0.5046339403095));
#309148=CARTESIAN_POINT('Ctrl Pts',(-2.80671098652772,-5.35999656574419,
-0.541556669620217));
#309149=CARTESIAN_POINT('Ctrl Pts',(-4.09440223185377,-4.45707223313806,
-0.61251961411017));
#309150=CARTESIAN_POINT('Ctrl Pts',(-4.64736815452183,-3.87708535521748,
-0.649638225160458));
#309151=CARTESIAN_POINT('Ctrl Pts',(-5.4847736324752,-2.55254213490508,
-0.723437752878511));
#309152=CARTESIAN_POINT('Ctrl Pts',(-5.76780330380029,-1.82501351119829,
-0.757622761511133));
#309153=CARTESIAN_POINT('Ctrl Pts',(-6.04426086165223,-0.290475166533927,
-0.830041704806752));
#309154=CARTESIAN_POINT('Ctrl Pts',(-6.03031629973367,0.502760525796865,
-0.867476605552441));
#309155=CARTESIAN_POINT('Ctrl Pts',(-5.69822517251945,2.03521656565479,
-0.939797279349468));
#309156=CARTESIAN_POINT('Ctrl Pts',(-5.38464996142156,2.75996713860472,
-0.974759009091658));
#309157=CARTESIAN_POINT('Ctrl Pts',(-4.50115627225226,4.04230360576368,
-1.04822554495606));
#309158=CARTESIAN_POINT('Ctrl Pts',(-3.94195716762769,4.5892824407932,-1.08375062569196));
#309159=CARTESIAN_POINT('Ctrl Pts',(-2.63174187997251,5.44998025903682,
-1.15510871084719));
#309160=CARTESIAN_POINT('Ctrl Pts',(-1.889514023902,5.7496100397065,-1.19279163926159));
#309161=CARTESIAN_POINT('Ctrl Pts',(-0.348527245563993,6.0398542003992,
-1.26618829883601));
#309162=CARTESIAN_POINT('Ctrl Pts',(0.434138257918517,6.03430450251552,
-1.30023510347325));
#309163=CARTESIAN_POINT('Ctrl Pts',(1.95932774100072,5.7245793778829,-1.37320683225349));
#309164=CARTESIAN_POINT('Ctrl Pts',(2.68696677606726,5.42126028600814,-1.41028877474877));
#309165=CARTESIAN_POINT('Ctrl Pts',(3.99277269973531,4.54774992880339,-1.48163580445412));
#309166=CARTESIAN_POINT('Ctrl Pts',(4.55632857822104,3.98299503126182,-1.51806926917442));
#309167=CARTESIAN_POINT('Ctrl Pts',(5.42285754322966,2.68154750848389,-1.59179487168831));
#309168=CARTESIAN_POINT('Ctrl Pts',(5.72298770964204,1.96099533051178,-1.62620541801734));
#309169=CARTESIAN_POINT('Ctrl Pts',(5.95935034168459,0.806412872961356,
-1.68069323307533));
#309170=CARTESIAN_POINT('Ctrl Pts',(6.,0.403234300545509,-1.69972030155839));
#309171=CARTESIAN_POINT('Ctrl Pts',(6.,1.03389519168218E-14,-1.71875));
#309172=CARTESIAN_POINT('Origin',(0.,8.67361737988403E-16,5.));
#309173=CARTESIAN_POINT('',(6.,2.1826494699417E-15,1.78125));
#309174=CARTESIAN_POINT('',(6.,1.60951317472757E-14,1.5625));
#309175=CARTESIAN_POINT('',(6.,1.32573658499991E-16,5.));
#309176=CARTESIAN_POINT('Ctrl Pts',(6.,-5.55111512312578E-15,-0.187499999999998));
#309177=CARTESIAN_POINT('Ctrl Pts',(6.,0.576081354367094,-0.160313189660176));
#309178=CARTESIAN_POINT('Ctrl Pts',(5.91702638582546,1.1503376579636,-0.133212508317213));
#309179=CARTESIAN_POINT('Ctrl Pts',(5.53219240607711,2.44889478307763,-0.0719301460114863));
#309180=CARTESIAN_POINT('Ctrl Pts',(5.16939551881057,3.14320557919123,-0.0358881017258123));
#309181=CARTESIAN_POINT('Ctrl Pts',(4.20118386713354,4.35294341729667,0.0371566471285775));
#309182=CARTESIAN_POINT('Ctrl Pts',(3.60575241514653,4.85763567656062,0.0715039495953657));
#309183=CARTESIAN_POINT('Ctrl Pts',(2.24408834398242,5.61993818487351,0.143736272976772));
#309184=CARTESIAN_POINT('Ctrl Pts',(1.48822218673184,5.86556326238038,0.181243759105709));
#309185=CARTESIAN_POINT('Ctrl Pts',(-0.068515577213796,6.05016071869312,
0.253806687248921));
#309186=CARTESIAN_POINT('Ctrl Pts',(-0.854081099803064,5.9899642220239,
0.288479978808746));
#309187=CARTESIAN_POINT('Ctrl Pts',(-2.3536877004239,5.57335017439412,0.361862270813308));
#309188=CARTESIAN_POINT('Ctrl Pts',(-3.05392899935969,5.22259080642952,
0.397816636184359));
#309189=CARTESIAN_POINT('Ctrl Pts',(-4.29634190905553,4.26286384933163,
0.468922163407154));
#309190=CARTESIAN_POINT('Ctrl Pts',(-4.8221635816438,3.65748698279963,0.506621093160949));
#309191=CARTESIAN_POINT('Ctrl Pts',(-5.59796976267574,2.29408392787543,
0.58019556420475));
#309192=CARTESIAN_POINT('Ctrl Pts',(-5.84708647207173,1.55295549233918,
0.614211902553629));
#309193=CARTESIAN_POINT('Ctrl Pts',(-6.05076398279004,0.00948217176010763,
0.687052511111859));
#309194=CARTESIAN_POINT('Ctrl Pts',(-6.00047413546166,-0.778593467100894,
0.72424389521885));
#309195=CARTESIAN_POINT('Ctrl Pts',(-5.59887394310715,-2.29632999880747,
0.795869916301666));
#309196=CARTESIAN_POINT('Ctrl Pts',(-5.24935217544605,-3.01079584896184,
0.831838609920422));
#309197=CARTESIAN_POINT('Ctrl Pts',(-4.30285973647881,-4.25249889353262,
0.905501307099982));
#309198=CARTESIAN_POINT('Ctrl Pts',(-3.71936449972661,-4.7712339531767,
0.940144686345269));
#309199=CARTESIAN_POINT('Ctrl Pts',(-2.37432149700639,-5.56642681405337,
1.0121106591994));
#309200=CARTESIAN_POINT('Ctrl Pts',(-1.6225717168347,-5.83007269088046,
1.04969619377305));
#309201=CARTESIAN_POINT('Ctrl Pts',(-0.0706144035415794,-6.04987811861958,
1.12255801108307));
#309202=CARTESIAN_POINT('Ctrl Pts',(0.714067011565161,-6.00800326027973,
1.15693267329168));
#309203=CARTESIAN_POINT('Ctrl Pts',(2.22264915056004,-5.62710306320001,
1.23019698636496));
#309204=CARTESIAN_POINT('Ctrl Pts',(2.93225948086817,-5.29207694793741,
1.26678866993634));
#309205=CARTESIAN_POINT('Ctrl Pts',(4.19898813659643,-4.35912259188468,
1.33754652637883));
#309206=CARTESIAN_POINT('Ctrl Pts',(4.73952956446563,-3.76433231500237,
1.37524957719054));
#309207=CARTESIAN_POINT('Ctrl Pts',(5.54571268861111,-2.41743703093539,
1.44903641764982));
#309208=CARTESIAN_POINT('Ctrl Pts',(5.81096626829843,-1.68274023662274,
1.48308701550236));
#309209=CARTESIAN_POINT('Ctrl Pts',(5.97649250358845,-0.61353127993814,
1.53354582813126));
#309210=CARTESIAN_POINT('Ctrl Pts',(6.,-0.306646382963594,1.54802854212027));
#309211=CARTESIAN_POINT('Ctrl Pts',(6.,2.77555756156289E-14,1.5625));
#309212=CARTESIAN_POINT('Ctrl Pts',(6.,1.49880108324396E-14,1.78125));
#309213=CARTESIAN_POINT('Ctrl Pts',(6.,-0.572678939529224,1.75422375866001));
#309214=CARTESIAN_POINT('Ctrl Pts',(5.91800369014654,-1.14358786020556,
1.72728104921443));
#309215=CARTESIAN_POINT('Ctrl Pts',(5.53635369796318,-2.43944113070009,
1.66612628899505));
#309216=CARTESIAN_POINT('Ctrl Pts',(5.17479590479424,-3.13428132315402,
1.63012862891726));
#309217=CARTESIAN_POINT('Ctrl Pts',(4.20441390584562,-4.35106713781484,
1.55675458711265));
#309218=CARTESIAN_POINT('Ctrl Pts',(3.60352824145776,-4.86039911440975,
1.52210592293855));
#309219=CARTESIAN_POINT('Ctrl Pts',(2.23436680393038,-5.62382857334181,
1.44952066142893));
#309220=CARTESIAN_POINT('Ctrl Pts',(1.47794603415836,-5.86817859973392,
1.41200687718543));
#309221=CARTESIAN_POINT('Ctrl Pts',(-0.0721756084407044,-6.04920383351369,
1.33979299456714));
#309222=CARTESIAN_POINT('Ctrl Pts',(-0.850441636930328,-5.98955870406894,
1.30542745698193));
#309223=CARTESIAN_POINT('Ctrl Pts',(-2.35818450799125,-5.57353001966035,
1.23168852223451));
#309224=CARTESIAN_POINT('Ctrl Pts',(-3.07136132076605,-5.21458358919537,
1.195144093216));
#309225=CARTESIAN_POINT('Ctrl Pts',(-4.30947960728758,-4.24709108315852,
1.12386120914637));
#309226=CARTESIAN_POINT('Ctrl Pts',(-4.82489175537719,-3.65099079453108,
1.08680520734935));
#309227=CARTESIAN_POINT('Ctrl Pts',(-5.59599279880615,-2.29923521512223,
1.01380594949795));
#309228=CARTESIAN_POINT('Ctrl Pts',(-5.84604828250109,-1.55735104566999,
0.979745535292359));
#309229=CARTESIAN_POINT('Ctrl Pts',(-6.05208909268611,-0.00297120746707236,
0.906390219177862));
#309230=CARTESIAN_POINT('Ctrl Pts',(-5.9995981480835,0.795412185708006,
0.868712384746716));
#309231=CARTESIAN_POINT('Ctrl Pts',(-5.59200466403976,2.30862617337791,
0.797299794537919));
#309232=CARTESIAN_POINT('Ctrl Pts',(-5.2474791233062,3.01069928691735,0.761863119915467));
#309233=CARTESIAN_POINT('Ctrl Pts',(-4.30577501001307,4.2512148277737,0.688378585303151));
#309234=CARTESIAN_POINT('Ctrl Pts',(-3.71513418603691,4.77601332690382,
0.653345745772946));
#309235=CARTESIAN_POINT('Ctrl Pts',(-2.36324112314454,5.57064612279665,
0.581080490070765));
#309236=CARTESIAN_POINT('Ctrl Pts',(-1.61444853991224,5.83185572665356,
0.543663212007828));
#309237=CARTESIAN_POINT('Ctrl Pts',(-0.0706927808031071,6.04924027915339,
0.471204808540938));
#309238=CARTESIAN_POINT('Ctrl Pts',(0.708908523410627,6.0079728699457,0.437048411347023));
#309239=CARTESIAN_POINT('Ctrl Pts',(2.21342193544873,5.63075564668377,0.364020424512322));
#309240=CARTESIAN_POINT('Ctrl Pts',(2.9236870728096,5.29683472622097,0.327380771732109));
#309241=CARTESIAN_POINT('Ctrl Pts',(4.19210437752919,4.36576624896074,0.256648075820155));
#309242=CARTESIAN_POINT('Ctrl Pts',(4.73366689496251,3.77172868347265,0.21894543912036));
#309243=CARTESIAN_POINT('Ctrl Pts',(5.54196569879411,2.42600175560982,0.145144518953668));
#309244=CARTESIAN_POINT('Ctrl Pts',(5.808342707209,1.69175542142419,0.111088435031726));
#309245=CARTESIAN_POINT('Ctrl Pts',(5.97601291190124,0.619751558434104,
0.0604977233453745));
#309246=CARTESIAN_POINT('Ctrl Pts',(6.,0.309758556663313,0.0458683296287967));
#309247=CARTESIAN_POINT('Ctrl Pts',(6.,2.63677968348475E-15,0.0312499999999991));
#309248=CARTESIAN_POINT('Origin',(0.,8.67361737988403E-16,5.));
#309249=CARTESIAN_POINT('',(6.,-2.57049285423475E-15,3.53125));
#309250=CARTESIAN_POINT('',(6.,2.60871389689021E-14,3.31250000000001));
#309251=CARTESIAN_POINT('',(6.,1.32573658499991E-16,5.));
#309252=CARTESIAN_POINT('',(-5.56513300460776,2.24260889167614,4.3));
#309253=CARTESIAN_POINT('Ctrl Pts',(-5.56513300460779,2.24260889167618,
4.29999999999994));
#309254=CARTESIAN_POINT('Ctrl Pts',(-5.29598978898201,2.91049966737262,
4.26703435210964));
#309255=CARTESIAN_POINT('Ctrl Pts',(-4.90881103715039,3.52449133733131,
4.23285234862231));
#309256=CARTESIAN_POINT('Ctrl Pts',(-3.89806696721271,4.62670295206297,
4.16273310160683));
#309257=CARTESIAN_POINT('Ctrl Pts',(-3.26813626689166,5.09122723636252,
4.12868632009684));
#309258=CARTESIAN_POINT('Ctrl Pts',(-1.85084558505042,5.76217410259774,
4.05528958373036));
#309259=CARTESIAN_POINT('Ctrl Pts',(-1.07425068762339,5.95603362377136,
4.01760664630479));
#309260=CARTESIAN_POINT('Ctrl Pts',(0.491642689492169,6.02982815809019,
3.94624866377506));
#309261=CARTESIAN_POINT('Ctrl Pts',(1.26554985762075,5.91599613957569,3.91072341508568));
#309262=CARTESIAN_POINT('Ctrl Pts',(2.73404541385783,5.39785774924788,3.83725691317482));
#309263=CARTESIAN_POINT('Ctrl Pts',(3.41372714253246,4.99583250130562,3.80229531421047));
#309264=CARTESIAN_POINT('Ctrl Pts',(4.58314192306331,3.95123953039067,3.72997453717357));
#309265=CARTESIAN_POINT('Ctrl Pts',(5.06067127023562,3.31769082048273,3.69253960393319));
#309266=CARTESIAN_POINT('Ctrl Pts',(5.7389811573739,1.91372004594514,3.62012073521678));
#309267=CARTESIAN_POINT('Ctrl Pts',(5.93763030254109,1.15877496180985,3.58593567047772));
#309268=CARTESIAN_POINT('Ctrl Pts',(5.99584573501727,0.257955583484155,
3.54342360963193));
#309269=CARTESIAN_POINT('Ctrl Pts',(6.,0.128908368236316,3.53733352853618));
#309270=CARTESIAN_POINT('Ctrl Pts',(6.,-1.2941037130787E-14,3.53125));
#309271=CARTESIAN_POINT('',(-6.,1.32573658499991E-16,4.3));
#309272=CARTESIAN_POINT('Origin',(0.,8.67361737988403E-16,4.3));
#309273=CARTESIAN_POINT('',(-5.51281765513596,-2.36829928456402,4.30000000000377));
#309274=CARTESIAN_POINT('Origin',(0.,8.67361737988403E-16,4.3));
#309275=CARTESIAN_POINT('Ctrl Pts',(6.,4.65599780952175E-14,3.31250000000001));
#309276=CARTESIAN_POINT('Ctrl Pts',(6.,0.383786548380919,3.33061190732474));
#309277=CARTESIAN_POINT('Ctrl Pts',(5.96317705814195,0.76760918361683,3.34872551768492));
#309278=CARTESIAN_POINT('Ctrl Pts',(5.74049833989295,1.91186775775114,3.40272612124355));
#309279=CARTESIAN_POINT('Ctrl Pts',(5.44357047524973,2.64122801660512,3.43734118463211));
#309280=CARTESIAN_POINT('Ctrl Pts',(4.58935776101163,3.94211204251619,3.51070363071812));
#309281=CARTESIAN_POINT('Ctrl Pts',(4.04147277688072,4.50208780601877,3.54676248963149));
#309282=CARTESIAN_POINT('Ctrl Pts',(2.7478864932634,5.39260451994447,3.61780907600754));
#309283=CARTESIAN_POINT('Ctrl Pts',(2.01058506327089,5.70863538339475,3.65551007466445));
#309284=CARTESIAN_POINT('Ctrl Pts',(0.475243583065782,6.03108562778345,
3.72912302902632));
#309285=CARTESIAN_POINT('Ctrl Pts',(-0.30640013799983,6.04201748954695,
3.76313936707741));
#309286=CARTESIAN_POINT('Ctrl Pts',(-1.83851098665274,5.76473566870732,
3.83594861519836));
#309287=CARTESIAN_POINT('Ctrl Pts',(-2.57387223944839,5.4760881030531,3.87316319334589));
#309288=CARTESIAN_POINT('Ctrl Pts',(-3.89624091234994,4.630229613505,3.94485035061565));
#309289=CARTESIAN_POINT('Ctrl Pts',(-4.46949934320597,4.07962684941699,
3.98072132995236));
#309290=CARTESIAN_POINT('Ctrl Pts',(-5.36284646836113,2.79970179088196,
4.05436912497271));
#309291=CARTESIAN_POINT('Ctrl Pts',(-5.67877217909002,2.08566338352181,
4.08907200122834));
#309292=CARTESIAN_POINT('Ctrl Pts',(-5.99112250266236,0.713090643414479,
4.15384735713948));
#309293=CARTESIAN_POINT('Ctrl Pts',(-6.03292388979285,0.0764271502393404,
4.18389319963645));
#309294=CARTESIAN_POINT('Ctrl Pts',(-5.91624513769634,-1.17978628549896,
4.24317725069079));
#309295=CARTESIAN_POINT('Ctrl Pts',(-5.76053056719885,-1.79168461261426,
4.27111370130226));
#309296=CARTESIAN_POINT('Ctrl Pts',(-5.51281765513233,-2.36829928456293,
4.30000000000162));
#309297=CARTESIAN_POINT('Origin',(2.99770677028732E-14,-1.99840144432528E-14,
-5.765625));
#309298=CARTESIAN_POINT('',(2.99770677028731E-14,-4.86334165753292,2.));
#309299=CARTESIAN_POINT('',(2.99770677028731E-14,-4.86334165753292,2.21875));
#309300=CARTESIAN_POINT('',(6.05497229851522E-14,-4.86334165753297,-5.765625));
#309301=CARTESIAN_POINT('Ctrl Pts',(-5.95587579405768E-16,-4.86334165753292,
2.21875));
#309302=CARTESIAN_POINT('Ctrl Pts',(1.58019549404244,-4.86334165753292,
2.30625));
#309303=CARTESIAN_POINT('Ctrl Pts',(2.85860050315749,-3.93452605039576,
2.39375));
#309304=CARTESIAN_POINT('Ctrl Pts',(4.13700551227253,-3.0057104432586,2.48125));
#309305=CARTESIAN_POINT('Ctrl Pts',(4.62531277436636,-1.5028552216293,2.56875));
#309306=CARTESIAN_POINT('Ctrl Pts',(5.11362003646019,7.95366714520796E-16,
2.65625));
#309307=CARTESIAN_POINT('Ctrl Pts',(4.62531277436636,1.5028552216293,2.74375));
#309308=CARTESIAN_POINT('Ctrl Pts',(4.13700551227253,3.0057104432586,2.83125));
#309309=CARTESIAN_POINT('Ctrl Pts',(2.85860050315749,3.93452605039576,2.91875));
#309310=CARTESIAN_POINT('Ctrl Pts',(1.58019549404244,4.86334165753292,3.00625));
#309311=CARTESIAN_POINT('Ctrl Pts',(0.,4.86334165753293,3.09375));
#309312=CARTESIAN_POINT('Ctrl Pts',(-0.613256677462664,4.86334165753293,
3.12770779793088));
#309313=CARTESIAN_POINT('Ctrl Pts',(-1.20731623616734,4.71110173778723,
3.16334165753294));
#309314=CARTESIAN_POINT('Ctrl Pts',(-5.95587579405768E-16,-4.86334165753292,
2.));
#309315=CARTESIAN_POINT('Ctrl Pts',(1.58019549404244,-4.86334165753292,
2.0875));
#309316=CARTESIAN_POINT('Ctrl Pts',(2.85860050315749,-3.93452605039576,
2.175));
#309317=CARTESIAN_POINT('Ctrl Pts',(4.13700551227253,-3.0057104432586,2.2625));
#309318=CARTESIAN_POINT('Ctrl Pts',(4.62531277436636,-1.5028552216293,2.35));
#309319=CARTESIAN_POINT('Ctrl Pts',(5.11362003646019,7.95366714520796E-16,
2.4375));
#309320=CARTESIAN_POINT('Ctrl Pts',(4.62531277436636,1.5028552216293,2.525));
#309321=CARTESIAN_POINT('Ctrl Pts',(4.13700551227253,3.0057104432586,2.6125));
#309322=CARTESIAN_POINT('Ctrl Pts',(2.85860050315749,3.93452605039576,2.7));
#309323=CARTESIAN_POINT('Ctrl Pts',(1.58019549404244,4.86334165753292,2.7875));
#309324=CARTESIAN_POINT('Ctrl Pts',(0.,4.86334165753293,2.875));
#309325=CARTESIAN_POINT('Ctrl Pts',(-1.58019549404244,4.86334165753292,
2.9625));
#309326=CARTESIAN_POINT('Ctrl Pts',(-2.85860050315749,3.93452605039576,
3.05));
#309327=CARTESIAN_POINT('Ctrl Pts',(-3.66754060707839,3.34679666228816,
3.10536763278335));
#309328=CARTESIAN_POINT('Ctrl Pts',(-4.17899100816594,2.48759446686254,
3.1633416575335));
#309329=CARTESIAN_POINT('Origin',(2.99770677028732E-14,-1.99840144432528E-14,
-5.765625));
#309330=CARTESIAN_POINT('',(2.99770677028731E-14,-4.86334165753292,0.25));
#309331=CARTESIAN_POINT('',(2.99770677028731E-14,-4.86334165753292,0.46875));
#309332=CARTESIAN_POINT('',(6.05497229851522E-14,-4.86334165753297,-5.765625));
#309333=CARTESIAN_POINT('Ctrl Pts',(-5.95587579405768E-16,-4.86334165753292,
0.46875));
#309334=CARTESIAN_POINT('Ctrl Pts',(1.58019549404244,-4.86334165753292,
0.556250000000001));
#309335=CARTESIAN_POINT('Ctrl Pts',(2.85860050315749,-3.93452605039576,
0.64375));
#309336=CARTESIAN_POINT('Ctrl Pts',(4.13700551227253,-3.0057104432586,0.731250000000001));
#309337=CARTESIAN_POINT('Ctrl Pts',(4.62531277436636,-1.5028552216293,0.81875));
#309338=CARTESIAN_POINT('Ctrl Pts',(5.11362003646019,7.95366714520796E-16,
0.906250000000001));
#309339=CARTESIAN_POINT('Ctrl Pts',(4.62531277436636,1.5028552216293,0.99375));
#309340=CARTESIAN_POINT('Ctrl Pts',(4.13700551227253,3.0057104432586,1.08125));
#309341=CARTESIAN_POINT('Ctrl Pts',(2.85860050315749,3.93452605039576,1.16875));
#309342=CARTESIAN_POINT('Ctrl Pts',(1.58019549404244,4.86334165753292,1.25625));
#309343=CARTESIAN_POINT('Ctrl Pts',(0.,4.86334165753293,1.34375));
#309344=CARTESIAN_POINT('Ctrl Pts',(-1.58019549404244,4.86334165753292,
1.43125));
#309345=CARTESIAN_POINT('Ctrl Pts',(-2.85860050315749,3.93452605039576,
1.51875));
#309346=CARTESIAN_POINT('Ctrl Pts',(-4.13700551227253,3.0057104432586,1.60625));
#309347=CARTESIAN_POINT('Ctrl Pts',(-4.62531277436636,1.5028552216293,1.69375));
#309348=CARTESIAN_POINT('Ctrl Pts',(-5.11362003646019,2.04784239646214E-15,
1.78125));
#309349=CARTESIAN_POINT('Ctrl Pts',(-4.62531277436636,-1.5028552216293,
1.86875));
#309350=CARTESIAN_POINT('Ctrl Pts',(-4.13700551227253,-3.00571044325859,
1.95625));
#309351=CARTESIAN_POINT('Ctrl Pts',(-2.85860050315749,-3.93452605039576,
2.04375));
#309352=CARTESIAN_POINT('Ctrl Pts',(-1.58019549404244,-4.86334165753292,
2.13125));
#309353=CARTESIAN_POINT('Ctrl Pts',(-5.95587579405768E-16,-4.86334165753292,
2.21875));
#309354=CARTESIAN_POINT('Ctrl Pts',(-5.95587579405768E-16,-4.86334165753292,
0.25));
#309355=CARTESIAN_POINT('Ctrl Pts',(1.58019549404244,-4.86334165753292,
0.337500000000001));
#309356=CARTESIAN_POINT('Ctrl Pts',(2.85860050315749,-3.93452605039576,
0.425));
#309357=CARTESIAN_POINT('Ctrl Pts',(4.13700551227253,-3.0057104432586,0.512500000000001));
#309358=CARTESIAN_POINT('Ctrl Pts',(4.62531277436636,-1.5028552216293,0.6));
#309359=CARTESIAN_POINT('Ctrl Pts',(5.11362003646019,7.95366714520796E-16,
0.687500000000001));
#309360=CARTESIAN_POINT('Ctrl Pts',(4.62531277436636,1.5028552216293,0.775));
#309361=CARTESIAN_POINT('Ctrl Pts',(4.13700551227253,3.0057104432586,0.8625));
#309362=CARTESIAN_POINT('Ctrl Pts',(2.85860050315749,3.93452605039576,0.95));
#309363=CARTESIAN_POINT('Ctrl Pts',(1.58019549404244,4.86334165753292,1.0375));
#309364=CARTESIAN_POINT('Ctrl Pts',(0.,4.86334165753293,1.125));
#309365=CARTESIAN_POINT('Ctrl Pts',(-1.58019549404244,4.86334165753292,
1.2125));
#309366=CARTESIAN_POINT('Ctrl Pts',(-2.85860050315749,3.93452605039576,
1.3));
#309367=CARTESIAN_POINT('Ctrl Pts',(-4.13700551227253,3.0057104432586,1.3875));
#309368=CARTESIAN_POINT('Ctrl Pts',(-4.62531277436636,1.5028552216293,1.475));
#309369=CARTESIAN_POINT('Ctrl Pts',(-5.11362003646019,2.04784239646214E-15,
1.5625));
#309370=CARTESIAN_POINT('Ctrl Pts',(-4.62531277436636,-1.5028552216293,
1.65));
#309371=CARTESIAN_POINT('Ctrl Pts',(-4.13700551227253,-3.00571044325859,
1.7375));
#309372=CARTESIAN_POINT('Ctrl Pts',(-2.85860050315749,-3.93452605039576,
1.825));
#309373=CARTESIAN_POINT('Ctrl Pts',(-1.58019549404244,-4.86334165753292,
1.9125));
#309374=CARTESIAN_POINT('Ctrl Pts',(-5.95587579405768E-16,-4.86334165753292,
2.));
#309375=CARTESIAN_POINT('Origin',(2.99770677028732E-14,-1.99840144432528E-14,
-5.765625));
#309376=CARTESIAN_POINT('',(2.99770677028731E-14,-4.86334165753292,-1.5));
#309377=CARTESIAN_POINT('',(2.99770677028731E-14,-4.86334165753292,-1.28125));
#309378=CARTESIAN_POINT('',(6.05497229851522E-14,-4.86334165753297,-5.765625));
#309379=CARTESIAN_POINT('Ctrl Pts',(-5.95587579405768E-16,-4.86334165753292,
-1.28125));
#309380=CARTESIAN_POINT('Ctrl Pts',(1.58019549404244,-4.86334165753292,
-1.19375));
#309381=CARTESIAN_POINT('Ctrl Pts',(2.85860050315749,-3.93452605039576,
-1.10625));
#309382=CARTESIAN_POINT('Ctrl Pts',(4.13700551227253,-3.0057104432586,-1.01875));
#309383=CARTESIAN_POINT('Ctrl Pts',(4.62531277436636,-1.5028552216293,-0.93125));
#309384=CARTESIAN_POINT('Ctrl Pts',(5.11362003646019,7.95366714520796E-16,
-0.843749999999999));
#309385=CARTESIAN_POINT('Ctrl Pts',(4.62531277436636,1.5028552216293,-0.75625));
#309386=CARTESIAN_POINT('Ctrl Pts',(4.13700551227253,3.0057104432586,-0.668749999999999));
#309387=CARTESIAN_POINT('Ctrl Pts',(2.85860050315749,3.93452605039576,-0.58125));
#309388=CARTESIAN_POINT('Ctrl Pts',(1.58019549404244,4.86334165753292,-0.49375));
#309389=CARTESIAN_POINT('Ctrl Pts',(0.,4.86334165753293,-0.40625));
#309390=CARTESIAN_POINT('Ctrl Pts',(-1.58019549404244,4.86334165753292,
-0.318749999999999));
#309391=CARTESIAN_POINT('Ctrl Pts',(-2.85860050315749,3.93452605039576,
-0.23125));
#309392=CARTESIAN_POINT('Ctrl Pts',(-4.13700551227253,3.0057104432586,-0.143749999999999));
#309393=CARTESIAN_POINT('Ctrl Pts',(-4.62531277436636,1.5028552216293,-0.056249999999999));
#309394=CARTESIAN_POINT('Ctrl Pts',(-5.11362003646019,2.04784239646214E-15,
0.0312500000000009));
#309395=CARTESIAN_POINT('Ctrl Pts',(-4.62531277436636,-1.5028552216293,
0.11875));
#309396=CARTESIAN_POINT('Ctrl Pts',(-4.13700551227253,-3.00571044325859,
0.20625));
#309397=CARTESIAN_POINT('Ctrl Pts',(-2.85860050315749,-3.93452605039576,
0.29375));
#309398=CARTESIAN_POINT('Ctrl Pts',(-1.58019549404244,-4.86334165753292,
0.381250000000001));
#309399=CARTESIAN_POINT('Ctrl Pts',(-5.95587579405768E-16,-4.86334165753292,
0.46875));
#309400=CARTESIAN_POINT('Ctrl Pts',(-5.95587579405768E-16,-4.86334165753292,
-1.5));
#309401=CARTESIAN_POINT('Ctrl Pts',(1.58019549404244,-4.86334165753292,
-1.4125));
#309402=CARTESIAN_POINT('Ctrl Pts',(2.85860050315749,-3.93452605039576,
-1.325));
#309403=CARTESIAN_POINT('Ctrl Pts',(4.13700551227253,-3.0057104432586,-1.2375));
#309404=CARTESIAN_POINT('Ctrl Pts',(4.62531277436636,-1.5028552216293,-1.15));
#309405=CARTESIAN_POINT('Ctrl Pts',(5.11362003646019,7.95366714520796E-16,
-1.0625));
#309406=CARTESIAN_POINT('Ctrl Pts',(4.62531277436636,1.5028552216293,-0.975));
#309407=CARTESIAN_POINT('Ctrl Pts',(4.13700551227253,3.0057104432586,-0.887499999999999));
#309408=CARTESIAN_POINT('Ctrl Pts',(2.85860050315749,3.93452605039576,-0.8));
#309409=CARTESIAN_POINT('Ctrl Pts',(1.58019549404244,4.86334165753292,-0.7125));
#309410=CARTESIAN_POINT('Ctrl Pts',(0.,4.86334165753293,-0.625));
#309411=CARTESIAN_POINT('Ctrl Pts',(-1.58019549404244,4.86334165753292,
-0.537499999999999));
#309412=CARTESIAN_POINT('Ctrl Pts',(-2.85860050315749,3.93452605039576,
-0.45));
#309413=CARTESIAN_POINT('Ctrl Pts',(-4.13700551227253,3.0057104432586,-0.362499999999999));
#309414=CARTESIAN_POINT('Ctrl Pts',(-4.62531277436636,1.5028552216293,-0.275));
#309415=CARTESIAN_POINT('Ctrl Pts',(-5.11362003646019,2.04784239646214E-15,
-0.187499999999999));
#309416=CARTESIAN_POINT('Ctrl Pts',(-4.62531277436636,-1.5028552216293,
-0.1));
#309417=CARTESIAN_POINT('Ctrl Pts',(-4.13700551227253,-3.00571044325859,
-0.0124999999999995));
#309418=CARTESIAN_POINT('Ctrl Pts',(-2.85860050315749,-3.93452605039576,
0.075));
#309419=CARTESIAN_POINT('Ctrl Pts',(-1.58019549404244,-4.86334165753292,
0.162500000000001));
#309420=CARTESIAN_POINT('Ctrl Pts',(-5.95587579405768E-16,-4.86334165753292,
0.25));
#309421=CARTESIAN_POINT('Origin',(2.99770677028732E-14,-1.99840144432528E-14,
-5.765625));
#309422=CARTESIAN_POINT('',(6.05497229851522E-14,-4.86334165753297,-3.16334165753295));
#309423=CARTESIAN_POINT('',(2.99770677028731E-14,-4.86334165753292,-3.03125));
#309424=CARTESIAN_POINT('',(6.05497229851522E-14,-4.86334165753297,-5.765625));
#309425=CARTESIAN_POINT('',(-2.21250112451954,-4.33092725081995,-3.16334165753294));
#309426=CARTESIAN_POINT('Origin',(2.99770677028732E-14,-1.99840144432528E-14,
-3.16334165753295));
#309427=CARTESIAN_POINT('Ctrl Pts',(-2.21250112451954,-4.33092725081995,
-3.16334165753294));
#309428=CARTESIAN_POINT('Ctrl Pts',(-1.17031043941251,-4.86334165753293,
-3.0960534776929));
#309429=CARTESIAN_POINT('Ctrl Pts',(-5.95587579405768E-16,-4.86334165753292,
-3.03125));
#309430=CARTESIAN_POINT('Ctrl Pts',(0.,6.09472152853892,-4.9453125));
#309431=CARTESIAN_POINT('Ctrl Pts',(-1.98029506767702,6.09472152853892,
-4.8578125));
#309432=CARTESIAN_POINT('Ctrl Pts',(-3.58238743130461,4.93073329257085,
-4.7703125));
#309433=CARTESIAN_POINT('Ctrl Pts',(-5.18447979493221,3.76674505660277,
-4.6828125));
#309434=CARTESIAN_POINT('Ctrl Pts',(-5.7964246247213,1.88337252830138,-4.5953125));
#309435=CARTESIAN_POINT('Ctrl Pts',(-6.40836945451038,2.1271229329878E-15,
-4.5078125));
#309436=CARTESIAN_POINT('Ctrl Pts',(-5.7964246247213,-1.88337252830138,
-4.4203125));
#309437=CARTESIAN_POINT('Ctrl Pts',(-5.18447979493221,-3.76674505660276,
-4.3328125));
#309438=CARTESIAN_POINT('Ctrl Pts',(-3.58238743130461,-4.93073329257084,
-4.2453125));
#309439=CARTESIAN_POINT('Ctrl Pts',(-1.98029506767702,-6.09472152853892,
-4.1578125));
#309440=CARTESIAN_POINT('Ctrl Pts',(-7.46388121161965E-16,-6.09472152853892,
-4.0703125));
#309441=CARTESIAN_POINT('Ctrl Pts',(1.98029506767702,-6.09472152853892,
-3.9828125));
#309442=CARTESIAN_POINT('Ctrl Pts',(3.58238743130461,-4.93073329257084,
-3.8953125));
#309443=CARTESIAN_POINT('Ctrl Pts',(5.18447979493221,-3.76674505660276,
-3.8078125));
#309444=CARTESIAN_POINT('Ctrl Pts',(5.7964246247213,-1.88337252830138,-3.7203125));
#309445=CARTESIAN_POINT('Ctrl Pts',(6.40836945451038,5.57525104943835E-16,
-3.6328125));
#309446=CARTESIAN_POINT('Ctrl Pts',(5.7964246247213,1.88337252830138,-3.5453125));
#309447=CARTESIAN_POINT('Ctrl Pts',(5.18447979493221,3.76674505660277,-3.4578125));
#309448=CARTESIAN_POINT('Ctrl Pts',(3.58238743130462,4.93073329257084,-3.3703125));
#309449=CARTESIAN_POINT('Ctrl Pts',(1.98029506767702,6.09472152853892,-3.2828125));
#309450=CARTESIAN_POINT('Ctrl Pts',(0.,6.09472152853892,-3.1953125));
#309451=CARTESIAN_POINT('Ctrl Pts',(-1.98029506767702,6.09472152853892,
-3.1078125));
#309452=CARTESIAN_POINT('Ctrl Pts',(-3.58238743130461,4.93073329257085,
-3.0203125));
#309453=CARTESIAN_POINT('Ctrl Pts',(-5.18447979493221,3.76674505660277,
-2.9328125));
#309454=CARTESIAN_POINT('Ctrl Pts',(-5.7964246247213,1.88337252830138,-2.8453125));
#309455=CARTESIAN_POINT('Ctrl Pts',(-6.40836945451038,2.1271229329878E-15,
-2.7578125));
#309456=CARTESIAN_POINT('Ctrl Pts',(-5.7964246247213,-1.88337252830138,
-2.6703125));
#309457=CARTESIAN_POINT('Ctrl Pts',(-5.18447979493221,-3.76674505660276,
-2.5828125));
#309458=CARTESIAN_POINT('Ctrl Pts',(-3.58238743130461,-4.93073329257084,
-2.4953125));
#309459=CARTESIAN_POINT('Ctrl Pts',(-1.98029506767702,-6.09472152853892,
-2.4078125));
#309460=CARTESIAN_POINT('Ctrl Pts',(-7.46388121161965E-16,-6.09472152853892,
-2.3203125));
#309461=CARTESIAN_POINT('Ctrl Pts',(1.98029506767702,-6.09472152853892,
-2.2328125));
#309462=CARTESIAN_POINT('Ctrl Pts',(3.58238743130461,-4.93073329257084,
-2.1453125));
#309463=CARTESIAN_POINT('Ctrl Pts',(5.18447979493221,-3.76674505660276,
-2.0578125));
#309464=CARTESIAN_POINT('Ctrl Pts',(5.7964246247213,-1.88337252830138,-1.9703125));
#309465=CARTESIAN_POINT('Ctrl Pts',(6.40836945451038,5.57525104943835E-16,
-1.8828125));
#309466=CARTESIAN_POINT('Ctrl Pts',(5.7964246247213,1.88337252830138,-1.7953125));
#309467=CARTESIAN_POINT('Ctrl Pts',(5.18447979493221,3.76674505660277,-1.7078125));
#309468=CARTESIAN_POINT('Ctrl Pts',(3.58238743130462,4.93073329257084,-1.6203125));
#309469=CARTESIAN_POINT('Ctrl Pts',(1.98029506767702,6.09472152853892,-1.5328125));
#309470=CARTESIAN_POINT('Ctrl Pts',(0.,6.09472152853892,-1.4453125));
#309471=CARTESIAN_POINT('Ctrl Pts',(-1.98029506767702,6.09472152853892,
-1.3578125));
#309472=CARTESIAN_POINT('Ctrl Pts',(-3.58238743130461,4.93073329257085,
-1.2703125));
#309473=CARTESIAN_POINT('Ctrl Pts',(-5.18447979493221,3.76674505660277,
-1.1828125));
#309474=CARTESIAN_POINT('Ctrl Pts',(-5.7964246247213,1.88337252830138,-1.0953125));
#309475=CARTESIAN_POINT('Ctrl Pts',(-6.40836945451038,2.1271229329878E-15,
-1.0078125));
#309476=CARTESIAN_POINT('Ctrl Pts',(-5.7964246247213,-1.88337252830138,
-0.9203125));
#309477=CARTESIAN_POINT('Ctrl Pts',(-5.18447979493221,-3.76674505660276,
-0.8328125));
#309478=CARTESIAN_POINT('Ctrl Pts',(-3.58238743130461,-4.93073329257084,
-0.7453125));
#309479=CARTESIAN_POINT('Ctrl Pts',(-1.98029506767702,-6.09472152853892,
-0.6578125));
#309480=CARTESIAN_POINT('Ctrl Pts',(-7.46388121161965E-16,-6.09472152853892,
-0.5703125));
#309481=CARTESIAN_POINT('Ctrl Pts',(1.98029506767702,-6.09472152853892,
-0.4828125));
#309482=CARTESIAN_POINT('Ctrl Pts',(3.58238743130461,-4.93073329257084,
-0.3953125));
#309483=CARTESIAN_POINT('Ctrl Pts',(5.18447979493221,-3.76674505660276,
-0.3078125));
#309484=CARTESIAN_POINT('Ctrl Pts',(5.7964246247213,-1.88337252830138,-0.2203125));
#309485=CARTESIAN_POINT('Ctrl Pts',(6.40836945451038,5.57525104943835E-16,
-0.1328125));
#309486=CARTESIAN_POINT('Ctrl Pts',(5.7964246247213,1.88337252830138,-0.0453125));
#309487=CARTESIAN_POINT('Ctrl Pts',(5.18447979493221,3.76674505660277,0.0421874999999997));
#309488=CARTESIAN_POINT('Ctrl Pts',(3.58238743130462,4.93073329257084,0.1296875));
#309489=CARTESIAN_POINT('Ctrl Pts',(1.98029506767702,6.09472152853892,0.217187499999999));
#309490=CARTESIAN_POINT('Ctrl Pts',(0.,6.09472152853892,0.3046875));
#309491=CARTESIAN_POINT('Ctrl Pts',(-1.98029506767702,6.09472152853892,
0.3921875));
#309492=CARTESIAN_POINT('Ctrl Pts',(-3.58238743130461,4.93073329257085,
0.4796875));
#309493=CARTESIAN_POINT('Ctrl Pts',(-5.18447979493221,3.76674505660277,
0.567187499999999));
#309494=CARTESIAN_POINT('Ctrl Pts',(-5.7964246247213,1.88337252830138,0.6546875));
#309495=CARTESIAN_POINT('Ctrl Pts',(-6.40836945451038,2.1271229329878E-15,
0.742187499999999));
#309496=CARTESIAN_POINT('Ctrl Pts',(-5.7964246247213,-1.88337252830138,
0.8296875));
#309497=CARTESIAN_POINT('Ctrl Pts',(-5.18447979493221,-3.76674505660276,
0.9171875));
#309498=CARTESIAN_POINT('Ctrl Pts',(-3.58238743130461,-4.93073329257084,
1.0046875));
#309499=CARTESIAN_POINT('Ctrl Pts',(-1.98029506767702,-6.09472152853892,
1.0921875));
#309500=CARTESIAN_POINT('Ctrl Pts',(-7.46388121161965E-16,-6.09472152853892,
1.1796875));
#309501=CARTESIAN_POINT('Ctrl Pts',(1.98029506767702,-6.09472152853892,
1.2671875));
#309502=CARTESIAN_POINT('Ctrl Pts',(3.58238743130461,-4.93073329257084,
1.3546875));
#309503=CARTESIAN_POINT('Ctrl Pts',(5.18447979493221,-3.76674505660276,
1.4421875));
#309504=CARTESIAN_POINT('Ctrl Pts',(5.7964246247213,-1.88337252830138,1.5296875));
#309505=CARTESIAN_POINT('Ctrl Pts',(6.40836945451038,5.57525104943835E-16,
1.6171875));
#309506=CARTESIAN_POINT('Ctrl Pts',(5.7964246247213,1.88337252830138,1.7046875));
#309507=CARTESIAN_POINT('Ctrl Pts',(5.18447979493221,3.76674505660277,1.7921875));
#309508=CARTESIAN_POINT('Ctrl Pts',(3.58238743130462,4.93073329257084,1.8796875));
#309509=CARTESIAN_POINT('Ctrl Pts',(1.98029506767702,6.09472152853892,1.9671875));
#309510=CARTESIAN_POINT('Ctrl Pts',(0.,6.09472152853892,2.0546875));
#309511=CARTESIAN_POINT('Ctrl Pts',(-1.98029506767702,6.09472152853892,
2.1421875));
#309512=CARTESIAN_POINT('Ctrl Pts',(-3.58238743130461,4.93073329257085,
2.2296875));
#309513=CARTESIAN_POINT('Ctrl Pts',(-5.18447979493221,3.76674505660277,
2.3171875));
#309514=CARTESIAN_POINT('Ctrl Pts',(-5.7964246247213,1.88337252830138,2.4046875));
#309515=CARTESIAN_POINT('Ctrl Pts',(-6.40836945451038,2.1271229329878E-15,
2.4921875));
#309516=CARTESIAN_POINT('Ctrl Pts',(-5.7964246247213,-1.88337252830138,
2.5796875));
#309517=CARTESIAN_POINT('Ctrl Pts',(-5.18447979493221,-3.76674505660276,
2.6671875));
#309518=CARTESIAN_POINT('Ctrl Pts',(-3.58238743130461,-4.93073329257084,
2.7546875));
#309519=CARTESIAN_POINT('Ctrl Pts',(-1.98029506767702,-6.09472152853892,
2.8421875));
#309520=CARTESIAN_POINT('Ctrl Pts',(-7.46388121161965E-16,-6.09472152853892,
2.9296875));
#309521=CARTESIAN_POINT('Ctrl Pts',(1.98029506767702,-6.09472152853892,
3.0171875));
#309522=CARTESIAN_POINT('Ctrl Pts',(3.58238743130461,-4.93073329257084,
3.1046875));
#309523=CARTESIAN_POINT('Ctrl Pts',(5.18447979493221,-3.76674505660276,
3.1921875));
#309524=CARTESIAN_POINT('Ctrl Pts',(5.7964246247213,-1.88337252830138,3.2796875));
#309525=CARTESIAN_POINT('Ctrl Pts',(6.40836945451038,5.57525104943835E-16,
3.3671875));
#309526=CARTESIAN_POINT('Ctrl Pts',(5.7964246247213,1.88337252830138,3.4546875));
#309527=CARTESIAN_POINT('Ctrl Pts',(5.18447979493221,3.76674505660277,3.5421875));
#309528=CARTESIAN_POINT('Ctrl Pts',(3.58238743130462,4.93073329257084,3.6296875));
#309529=CARTESIAN_POINT('Ctrl Pts',(1.98029506767702,6.09472152853892,3.7171875));
#309530=CARTESIAN_POINT('Ctrl Pts',(0.,6.09472152853892,3.8046875));
#309531=CARTESIAN_POINT('Ctrl Pts',(-1.98029506767702,6.09472152853892,
3.8921875));
#309532=CARTESIAN_POINT('Ctrl Pts',(-3.58238743130461,4.93073329257085,
3.9796875));
#309533=CARTESIAN_POINT('Ctrl Pts',(-5.18447979493221,3.76674505660277,
4.0671875));
#309534=CARTESIAN_POINT('Ctrl Pts',(-5.7964246247213,1.88337252830138,4.1546875));
#309535=CARTESIAN_POINT('Ctrl Pts',(-6.40836945451038,2.1271229329878E-15,
4.2421875));
#309536=CARTESIAN_POINT('Ctrl Pts',(-5.7964246247213,-1.88337252830138,
4.3296875));
#309537=CARTESIAN_POINT('Ctrl Pts',(-5.18447979493221,-3.76674505660276,
4.4171875));
#309538=CARTESIAN_POINT('Ctrl Pts',(-3.58238743130461,-4.93073329257084,
4.5046875));
#309539=CARTESIAN_POINT('Ctrl Pts',(-1.98029506767702,-6.09472152853892,
4.5921875));
#309540=CARTESIAN_POINT('Ctrl Pts',(-7.46388121161965E-16,-6.09472152853892,
4.6796875));
#309541=CARTESIAN_POINT('Ctrl Pts',(1.98029506767702,-6.09472152853892,
4.7671875));
#309542=CARTESIAN_POINT('Ctrl Pts',(3.58238743130461,-4.93073329257084,
4.8546875));
#309543=CARTESIAN_POINT('Ctrl Pts',(5.18447979493221,-3.76674505660276,
4.9421875));
#309544=CARTESIAN_POINT('Ctrl Pts',(5.7964246247213,-1.88337252830138,5.0296875));
#309545=CARTESIAN_POINT('Ctrl Pts',(6.40836945451038,5.57525104943835E-16,
5.1171875));
#309546=CARTESIAN_POINT('Ctrl Pts',(5.7964246247213,1.88337252830138,5.2046875));
#309547=CARTESIAN_POINT('Ctrl Pts',(5.18447979493221,3.76674505660277,5.2921875));
#309548=CARTESIAN_POINT('Ctrl Pts',(3.58238743130462,4.93073329257084,5.3796875));
#309549=CARTESIAN_POINT('Ctrl Pts',(1.98029506767702,6.09472152853892,5.4671875));
#309550=CARTESIAN_POINT('Ctrl Pts',(0.,6.09472152853892,5.5546875));
#309551=CARTESIAN_POINT('Ctrl Pts',(-1.98029506767702,6.09472152853892,
5.6421875));
#309552=CARTESIAN_POINT('Ctrl Pts',(-3.58238743130461,4.93073329257085,
5.7296875));
#309553=CARTESIAN_POINT('Ctrl Pts',(-5.18447979493221,3.76674505660277,
5.81718749999999));
#309554=CARTESIAN_POINT('Ctrl Pts',(-5.7964246247213,1.88337252830138,5.9046875));
#309555=CARTESIAN_POINT('Ctrl Pts',(-6.40836945451038,2.1271229329878E-15,
5.9921875));
#309556=CARTESIAN_POINT('Ctrl Pts',(-5.7964246247213,-1.88337252830138,
6.0796875));
#309557=CARTESIAN_POINT('Ctrl Pts',(-5.18447979493221,-3.76674505660276,
6.1671875));
#309558=CARTESIAN_POINT('Ctrl Pts',(-3.58238743130461,-4.93073329257084,
6.2546875));
#309559=CARTESIAN_POINT('Ctrl Pts',(-1.98029506767702,-6.09472152853892,
6.3421875));
#309560=CARTESIAN_POINT('Ctrl Pts',(-7.46388121161965E-16,-6.09472152853892,
6.4296875));
#309561=CARTESIAN_POINT('Ctrl Pts',(1.98029506767702,-6.09472152853892,
6.5171875));
#309562=CARTESIAN_POINT('Ctrl Pts',(3.58238743130461,-4.93073329257084,
6.6046875));
#309563=CARTESIAN_POINT('Ctrl Pts',(5.18447979493221,-3.76674505660276,
6.69218749999999));
#309564=CARTESIAN_POINT('Ctrl Pts',(5.7964246247213,-1.88337252830138,6.7796875));
#309565=CARTESIAN_POINT('Ctrl Pts',(5.88101053842786,-1.6230438542098,6.79178216456621));
#309566=CARTESIAN_POINT('Ctrl Pts',(5.94191924599894,-1.35618073443886,
6.80418041431716));
#309567=CARTESIAN_POINT('Ctrl Pts',(0.,4.8633208818601,-5.6562619948403));
#309568=CARTESIAN_POINT('Ctrl Pts',(-1.58018874361713,4.86332088186009,
-5.5687619948403));
#309569=CARTESIAN_POINT('Ctrl Pts',(-2.85858829152339,3.93450924252337,
-5.4812619948403));
#309570=CARTESIAN_POINT('Ctrl Pts',(-4.13698783942964,3.00569760318665,
-5.39376199484029));
#309571=CARTESIAN_POINT('Ctrl Pts',(-4.62529301552733,1.50284880159333,
-5.3062619948403));
#309572=CARTESIAN_POINT('Ctrl Pts',(-5.11359819162502,2.04784105885177E-15,
-5.2187619948403));
#309573=CARTESIAN_POINT('Ctrl Pts',(-4.62529301552733,-1.50284880159332,
-5.1312619948403));
#309574=CARTESIAN_POINT('Ctrl Pts',(-4.13698783942964,-3.00569760318664,
-5.0437619948403));
#309575=CARTESIAN_POINT('Ctrl Pts',(-2.85858829152339,-3.93450924252337,
-4.9562619948403));
#309576=CARTESIAN_POINT('Ctrl Pts',(-1.58018874361713,-4.86332088186009,
-4.8687619948403));
#309577=CARTESIAN_POINT('Ctrl Pts',(-5.95585035119645E-16,-4.86332088186009,
-4.7812619948403));
#309578=CARTESIAN_POINT('Ctrl Pts',(1.58018874361713,-4.86332088186009,
-4.6937619948403));
#309579=CARTESIAN_POINT('Ctrl Pts',(2.85858829152339,-3.93450924252337,
-4.6062619948403));
#309580=CARTESIAN_POINT('Ctrl Pts',(4.13698783942964,-3.00569760318665,
-4.5187619948403));
#309581=CARTESIAN_POINT('Ctrl Pts',(4.62529301552733,-1.50284880159333,
-4.4312619948403));
#309582=CARTESIAN_POINT('Ctrl Pts',(5.11359819162502,7.95370727351915E-16,
-4.3437619948403));
#309583=CARTESIAN_POINT('Ctrl Pts',(4.62529301552733,1.50284880159333,-4.2562619948403));
#309584=CARTESIAN_POINT('Ctrl Pts',(4.13698783942964,3.00569760318665,-4.1687619948403));
#309585=CARTESIAN_POINT('Ctrl Pts',(2.85858829152339,3.93450924252337,-4.0812619948403));
#309586=CARTESIAN_POINT('Ctrl Pts',(1.58018874361713,4.86332088186009,-3.9937619948403));
#309587=CARTESIAN_POINT('Ctrl Pts',(0.,4.8633208818601,-3.9062619948403));
#309588=CARTESIAN_POINT('Ctrl Pts',(-1.58018874361713,4.86332088186009,
-3.8187619948403));
#309589=CARTESIAN_POINT('Ctrl Pts',(-2.85858829152339,3.93450924252337,
-3.7312619948403));
#309590=CARTESIAN_POINT('Ctrl Pts',(-4.13698783942964,3.00569760318665,
-3.6437619948403));
#309591=CARTESIAN_POINT('Ctrl Pts',(-4.62529301552733,1.50284880159333,
-3.5562619948403));
#309592=CARTESIAN_POINT('Ctrl Pts',(-5.11359819162502,2.04784105885177E-15,
-3.4687619948403));
#309593=CARTESIAN_POINT('Ctrl Pts',(-4.62529301552733,-1.50284880159332,
-3.3812619948403));
#309594=CARTESIAN_POINT('Ctrl Pts',(-4.13698783942964,-3.00569760318664,
-3.2937619948403));
#309595=CARTESIAN_POINT('Ctrl Pts',(-2.85858829152339,-3.93450924252337,
-3.2062619948403));
#309596=CARTESIAN_POINT('Ctrl Pts',(-1.58018874361713,-4.86332088186009,
-3.1187619948403));
#309597=CARTESIAN_POINT('Ctrl Pts',(-5.95585035119645E-16,-4.86332088186009,
-3.0312619948403));
#309598=CARTESIAN_POINT('Ctrl Pts',(1.58018874361713,-4.86332088186009,
-2.9437619948403));
#309599=CARTESIAN_POINT('Ctrl Pts',(2.85858829152339,-3.93450924252337,
-2.8562619948403));
#309600=CARTESIAN_POINT('Ctrl Pts',(4.13698783942964,-3.00569760318665,
-2.7687619948403));
#309601=CARTESIAN_POINT('Ctrl Pts',(4.62529301552733,-1.50284880159333,
-2.6812619948403));
#309602=CARTESIAN_POINT('Ctrl Pts',(5.11359819162502,7.95370727351915E-16,
-2.5937619948403));
#309603=CARTESIAN_POINT('Ctrl Pts',(4.62529301552733,1.50284880159333,-2.5062619948403));
#309604=CARTESIAN_POINT('Ctrl Pts',(4.13698783942964,3.00569760318665,-2.4187619948403));
#309605=CARTESIAN_POINT('Ctrl Pts',(2.85858829152339,3.93450924252337,-2.3312619948403));
#309606=CARTESIAN_POINT('Ctrl Pts',(1.58018874361713,4.86332088186009,-2.2437619948403));
#309607=CARTESIAN_POINT('Ctrl Pts',(0.,4.8633208818601,-2.1562619948403));
#309608=CARTESIAN_POINT('Ctrl Pts',(-1.58018874361713,4.86332088186009,
-2.0687619948403));
#309609=CARTESIAN_POINT('Ctrl Pts',(-2.85858829152339,3.93450924252337,
-1.9812619948403));
#309610=CARTESIAN_POINT('Ctrl Pts',(-4.13698783942964,3.00569760318665,
-1.8937619948403));
#309611=CARTESIAN_POINT('Ctrl Pts',(-4.62529301552733,1.50284880159333,
-1.8062619948403));
#309612=CARTESIAN_POINT('Ctrl Pts',(-5.11359819162502,2.04784105885177E-15,
-1.7187619948403));
#309613=CARTESIAN_POINT('Ctrl Pts',(-4.62529301552733,-1.50284880159332,
-1.6312619948403));
#309614=CARTESIAN_POINT('Ctrl Pts',(-4.13698783942964,-3.00569760318664,
-1.5437619948403));
#309615=CARTESIAN_POINT('Ctrl Pts',(-2.85858829152339,-3.93450924252337,
-1.4562619948403));
#309616=CARTESIAN_POINT('Ctrl Pts',(-1.58018874361713,-4.86332088186009,
-1.3687619948403));
#309617=CARTESIAN_POINT('Ctrl Pts',(-5.95585035119645E-16,-4.86332088186009,
-1.2812619948403));
#309618=CARTESIAN_POINT('Ctrl Pts',(1.58018874361713,-4.86332088186009,
-1.1937619948403));
#309619=CARTESIAN_POINT('Ctrl Pts',(2.85858829152339,-3.93450924252337,
-1.1062619948403));
#309620=CARTESIAN_POINT('Ctrl Pts',(4.13698783942964,-3.00569760318665,
-1.0187619948403));
#309621=CARTESIAN_POINT('Ctrl Pts',(4.62529301552733,-1.50284880159333,
-0.931261994840301));
#309622=CARTESIAN_POINT('Ctrl Pts',(5.11359819162502,7.95370727351915E-16,
-0.8437619948403));
#309623=CARTESIAN_POINT('Ctrl Pts',(4.62529301552733,1.50284880159333,-0.756261994840301));
#309624=CARTESIAN_POINT('Ctrl Pts',(4.13698783942964,3.00569760318665,-0.6687619948403));
#309625=CARTESIAN_POINT('Ctrl Pts',(2.85858829152339,3.93450924252337,-0.581261994840301));
#309626=CARTESIAN_POINT('Ctrl Pts',(1.58018874361713,4.86332088186009,-0.493761994840301));
#309627=CARTESIAN_POINT('Ctrl Pts',(0.,4.8633208818601,-0.406261994840301));
#309628=CARTESIAN_POINT('Ctrl Pts',(-1.58018874361713,4.86332088186009,
-0.3187619948403));
#309629=CARTESIAN_POINT('Ctrl Pts',(-2.85858829152339,3.93450924252337,
-0.231261994840301));
#309630=CARTESIAN_POINT('Ctrl Pts',(-4.13698783942964,3.00569760318665,
-0.1437619948403));
#309631=CARTESIAN_POINT('Ctrl Pts',(-4.62529301552733,1.50284880159333,
-0.0562619948403003));
#309632=CARTESIAN_POINT('Ctrl Pts',(-5.11359819162502,2.04784105885177E-15,
0.0312380051596996));
#309633=CARTESIAN_POINT('Ctrl Pts',(-4.62529301552733,-1.50284880159332,
0.118738005159699));
#309634=CARTESIAN_POINT('Ctrl Pts',(-4.13698783942964,-3.00569760318664,
0.206238005159699));
#309635=CARTESIAN_POINT('Ctrl Pts',(-2.85858829152339,-3.93450924252337,
0.293738005159699));
#309636=CARTESIAN_POINT('Ctrl Pts',(-1.58018874361713,-4.86332088186009,
0.3812380051597));
#309637=CARTESIAN_POINT('Ctrl Pts',(-5.95585035119645E-16,-4.86332088186009,
0.468738005159699));
#309638=CARTESIAN_POINT('Ctrl Pts',(1.58018874361713,-4.86332088186009,
0.5562380051597));
#309639=CARTESIAN_POINT('Ctrl Pts',(2.85858829152339,-3.93450924252337,
0.643738005159699));
#309640=CARTESIAN_POINT('Ctrl Pts',(4.13698783942964,-3.00569760318665,
0.7312380051597));
#309641=CARTESIAN_POINT('Ctrl Pts',(4.62529301552733,-1.50284880159333,
0.818738005159699));
#309642=CARTESIAN_POINT('Ctrl Pts',(5.11359819162502,7.95370727351915E-16,
0.9062380051597));
#309643=CARTESIAN_POINT('Ctrl Pts',(4.62529301552733,1.50284880159333,0.993738005159699));
#309644=CARTESIAN_POINT('Ctrl Pts',(4.13698783942964,3.00569760318665,1.0812380051597));
#309645=CARTESIAN_POINT('Ctrl Pts',(2.85858829152339,3.93450924252337,1.1687380051597));
#309646=CARTESIAN_POINT('Ctrl Pts',(1.58018874361713,4.86332088186009,1.2562380051597));
#309647=CARTESIAN_POINT('Ctrl Pts',(0.,4.8633208818601,1.3437380051597));
#309648=CARTESIAN_POINT('Ctrl Pts',(-1.58018874361713,4.86332088186009,
1.4312380051597));
#309649=CARTESIAN_POINT('Ctrl Pts',(-2.85858829152339,3.93450924252337,
1.5187380051597));
#309650=CARTESIAN_POINT('Ctrl Pts',(-4.13698783942964,3.00569760318665,
1.6062380051597));
#309651=CARTESIAN_POINT('Ctrl Pts',(-4.62529301552733,1.50284880159333,
1.6937380051597));
#309652=CARTESIAN_POINT('Ctrl Pts',(-5.11359819162502,2.04784105885177E-15,
1.7812380051597));
#309653=CARTESIAN_POINT('Ctrl Pts',(-4.62529301552733,-1.50284880159332,
1.8687380051597));
#309654=CARTESIAN_POINT('Ctrl Pts',(-4.13698783942964,-3.00569760318664,
1.9562380051597));
#309655=CARTESIAN_POINT('Ctrl Pts',(-2.85858829152339,-3.93450924252337,
2.0437380051597));
#309656=CARTESIAN_POINT('Ctrl Pts',(-1.58018874361713,-4.86332088186009,
2.1312380051597));
#309657=CARTESIAN_POINT('Ctrl Pts',(-5.95585035119645E-16,-4.86332088186009,
2.2187380051597));
#309658=CARTESIAN_POINT('Ctrl Pts',(1.58018874361713,-4.86332088186009,
2.3062380051597));
#309659=CARTESIAN_POINT('Ctrl Pts',(2.85858829152339,-3.93450924252337,
2.3937380051597));
#309660=CARTESIAN_POINT('Ctrl Pts',(4.13698783942964,-3.00569760318665,
2.4812380051597));
#309661=CARTESIAN_POINT('Ctrl Pts',(4.62529301552733,-1.50284880159333,
2.5687380051597));
#309662=CARTESIAN_POINT('Ctrl Pts',(5.11359819162502,7.95370727351915E-16,
2.6562380051597));
#309663=CARTESIAN_POINT('Ctrl Pts',(4.62529301552733,1.50284880159333,2.7437380051597));
#309664=CARTESIAN_POINT('Ctrl Pts',(4.13698783942964,3.00569760318665,2.8312380051597));
#309665=CARTESIAN_POINT('Ctrl Pts',(2.85858829152339,3.93450924252337,2.9187380051597));
#309666=CARTESIAN_POINT('Ctrl Pts',(1.58018874361713,4.86332088186009,3.0062380051597));
#309667=CARTESIAN_POINT('Ctrl Pts',(0.,4.8633208818601,3.0937380051597));
#309668=CARTESIAN_POINT('Ctrl Pts',(-1.58018874361713,4.86332088186009,
3.1812380051597));
#309669=CARTESIAN_POINT('Ctrl Pts',(-2.85858829152339,3.93450924252337,
3.2687380051597));
#309670=CARTESIAN_POINT('Ctrl Pts',(-4.13698783942964,3.00569760318665,
3.3562380051597));
#309671=CARTESIAN_POINT('Ctrl Pts',(-4.62529301552733,1.50284880159333,
3.4437380051597));
#309672=CARTESIAN_POINT('Ctrl Pts',(-5.11359819162502,2.04784105885177E-15,
3.5312380051597));
#309673=CARTESIAN_POINT('Ctrl Pts',(-4.62529301552733,-1.50284880159332,
3.6187380051597));
#309674=CARTESIAN_POINT('Ctrl Pts',(-4.13698783942964,-3.00569760318664,
3.7062380051597));
#309675=CARTESIAN_POINT('Ctrl Pts',(-2.85858829152339,-3.93450924252337,
3.7937380051597));
#309676=CARTESIAN_POINT('Ctrl Pts',(-1.58018874361713,-4.86332088186009,
3.8812380051597));
#309677=CARTESIAN_POINT('Ctrl Pts',(-5.95585035119645E-16,-4.86332088186009,
3.9687380051597));
#309678=CARTESIAN_POINT('Ctrl Pts',(1.58018874361713,-4.86332088186009,
4.0562380051597));
#309679=CARTESIAN_POINT('Ctrl Pts',(2.85858829152339,-3.93450924252337,
4.1437380051597));
#309680=CARTESIAN_POINT('Ctrl Pts',(4.13698783942964,-3.00569760318665,
4.2312380051597));
#309681=CARTESIAN_POINT('Ctrl Pts',(4.62529301552733,-1.50284880159333,
4.3187380051597));
#309682=CARTESIAN_POINT('Ctrl Pts',(5.11359819162502,7.95370727351915E-16,
4.4062380051597));
#309683=CARTESIAN_POINT('Ctrl Pts',(4.62529301552733,1.50284880159333,4.4937380051597));
#309684=CARTESIAN_POINT('Ctrl Pts',(4.13698783942964,3.00569760318665,4.5812380051597));
#309685=CARTESIAN_POINT('Ctrl Pts',(2.85858829152339,3.93450924252337,4.6687380051597));
#309686=CARTESIAN_POINT('Ctrl Pts',(1.58018874361713,4.86332088186009,4.7562380051597));
#309687=CARTESIAN_POINT('Ctrl Pts',(0.,4.8633208818601,4.8437380051597));
#309688=CARTESIAN_POINT('Ctrl Pts',(-1.58018874361713,4.86332088186009,
4.9312380051597));
#309689=CARTESIAN_POINT('Ctrl Pts',(-2.85858829152339,3.93450924252337,
5.0187380051597));
#309690=CARTESIAN_POINT('Ctrl Pts',(-4.13698783942964,3.00569760318665,
5.1062380051597));
#309691=CARTESIAN_POINT('Ctrl Pts',(-4.62529301552733,1.50284880159333,
5.1937380051597));
#309692=CARTESIAN_POINT('Ctrl Pts',(-5.11359819162502,2.04784105885177E-15,
5.2812380051597));
#309693=CARTESIAN_POINT('Ctrl Pts',(-4.62529301552733,-1.50284880159332,
5.3687380051597));
#309694=CARTESIAN_POINT('Ctrl Pts',(-4.13698783942964,-3.00569760318664,
5.45623800515969));
#309695=CARTESIAN_POINT('Ctrl Pts',(-2.85858829152339,-3.93450924252337,
5.5437380051597));
#309696=CARTESIAN_POINT('Ctrl Pts',(-1.58018874361713,-4.86332088186009,
5.6312380051597));
#309697=CARTESIAN_POINT('Ctrl Pts',(-5.95585035119645E-16,-4.86332088186009,
5.7187380051597));
#309698=CARTESIAN_POINT('Ctrl Pts',(1.58018874361713,-4.86332088186009,
5.8062380051597));
#309699=CARTESIAN_POINT('Ctrl Pts',(2.85858829152339,-3.93450924252337,
5.8937380051597));
#309700=CARTESIAN_POINT('Ctrl Pts',(4.13698783942964,-3.00569760318665,
5.9812380051597));
#309701=CARTESIAN_POINT('Ctrl Pts',(4.62529301552733,-1.50284880159333,
6.0687380051597));
#309702=CARTESIAN_POINT('Ctrl Pts',(4.69278887050841,-1.2951179198905,6.0808326697259));
#309703=CARTESIAN_POINT('Ctrl Pts',(4.74139135185731,-1.08217283668972,
6.09323091947686));
#309704=CARTESIAN_POINT('Ctrl Pts',(6.,2.65065747129256E-14,1.5625));
#309705=CARTESIAN_POINT('Ctrl Pts',(6.,0.473732133569272,1.58485667856562));
#309706=CARTESIAN_POINT('Ctrl Pts',(5.94389257800599,0.946895016021675,
1.6071864926588));
#309707=CARTESIAN_POINT('Ctrl Pts',(5.64770904370383,2.17244600347447,1.66502350127759));
#309708=CARTESIAN_POINT('Ctrl Pts',(5.31536957028271,2.89188711817904,1.70046744841851));
#309709=CARTESIAN_POINT('Ctrl Pts',(4.39895257827164,4.15311566791862,1.77404135550628));
#309710=CARTESIAN_POINT('Ctrl Pts',(3.82704939643144,4.68538294493608,1.80905948364897));
#309711=CARTESIAN_POINT('Ctrl Pts',(2.49846473521043,5.51207511269938,1.88074612354776));
#309712=CARTESIAN_POINT('Ctrl Pts',(1.7510721703992,5.79301286248726,1.91838826687317));
#309713=CARTESIAN_POINT('Ctrl Pts',(0.204147040411568,6.04663706712432,
1.99151741577544));
#309714=CARTESIAN_POINT('Ctrl Pts',(-0.579605426814209,6.02225380331358,
2.02568982903828));
#309715=CARTESIAN_POINT('Ctrl Pts',(-2.09637414501486,5.67557241238266,
2.09882255514758));
#309716=CARTESIAN_POINT('Ctrl Pts',(-2.81483629742654,5.35571705240381,
2.13573376658461));
#309717=CARTESIAN_POINT('Ctrl Pts',(-4.10127598593334,4.45079123039165,
2.20666972598103));
#309718=CARTESIAN_POINT('Ctrl Pts',(-4.65351072191004,3.86976109467243,
2.24383825254408));
#309719=CARTESIAN_POINT('Ctrl Pts',(-5.48891111541853,2.54363857790455,
2.31764245793256));
#309720=CARTESIAN_POINT('Ctrl Pts',(-5.7707654703417,1.81563335639617,2.35181543594963));
#309721=CARTESIAN_POINT('Ctrl Pts',(-6.04470409317909,0.280751068370845,
2.42425061084664));
#309722=CARTESIAN_POINT('Ctrl Pts',(-6.02949439172197,-0.512333236812288,
2.46167836723043));
#309723=CARTESIAN_POINT('Ctrl Pts',(-5.69499213987656,-2.04431033388393,
2.53397643844432));
#309724=CARTESIAN_POINT('Ctrl Pts',(-5.38018169086334,-2.76871518145314,
2.56896695243465));
#309725=CARTESIAN_POINT('Ctrl Pts',(-4.49451807829644,-4.04966880786669,
2.64244088373343));
#309726=CARTESIAN_POINT('Ctrl Pts',(-3.93448113525675,-4.59568124109636,
2.67792948743115));
#309727=CARTESIAN_POINT('Ctrl Pts',(-2.62304423346144,-5.45415327610023,
2.7493099428143));
#309728=CARTESIAN_POINT('Ctrl Pts',(-1.88046359937015,-5.75255908400189,
2.78699085532114));
#309729=CARTESIAN_POINT('Ctrl Pts',(-0.339071917529684,-6.04040283393684,
2.86037068214262));
#309730=CARTESIAN_POINT('Ctrl Pts',(0.443667288736679,-6.03362176991941,
2.89442275038474));
#309731=CARTESIAN_POINT('Ctrl Pts',(1.96832289167546,-5.72147630793342,
2.96740581367033));
#309732=CARTESIAN_POINT('Ctrl Pts',(2.69537329403833,-5.41706837063913,
3.00447721562741));
#309733=CARTESIAN_POINT('Ctrl Pts',(3.99992726994981,-4.54149783876324,
3.07579809851961));
#309734=CARTESIAN_POINT('Ctrl Pts',(4.5627506802707,-3.97568211547479,3.11227661747247));
#309735=CARTESIAN_POINT('Ctrl Pts',(5.42726028909776,-2.67262381178519,
3.18600770383688));
#309736=CARTESIAN_POINT('Ctrl Pts',(5.72620297456507,-1.95158464272292,
3.22039953338864));
#309737=CARTESIAN_POINT('Ctrl Pts',(5.96001028500831,-0.799856624140742,
3.27475263988459));
#309738=CARTESIAN_POINT('Ctrl Pts',(6.,-0.39994790712138,3.29362539519932));
#309739=CARTESIAN_POINT('Ctrl Pts',(6.,4.85722573273506E-14,3.31250000000001));
#309740=CARTESIAN_POINT('Ctrl Pts',(-5.51281765513598,-2.36829928456402,
4.30000000000379));
#309741=CARTESIAN_POINT('Ctrl Pts',(-5.65503173457777,-1.9040941811954,
4.24743727896327));
#309742=CARTESIAN_POINT('Ctrl Pts',(-5.79869704924777,-1.24715028022825,
4.17742481762423));
#309743=CARTESIAN_POINT('Ctrl Pts',(-5.76255122889151,-0.295979987394846,
4.06824939279623));
#309744=CARTESIAN_POINT('Ctrl Pts',(-5.75106682344018,-0.147589105085812,
4.05106682344018));
#309745=CARTESIAN_POINT('Ctrl Pts',(-5.73382214207426,-1.18860743158296E-14,
4.03382214207426));
#309746=CARTESIAN_POINT('Ctrl Pts',(-5.95587579405768E-16,-4.86334165753292,
-3.03125));
#309747=CARTESIAN_POINT('Ctrl Pts',(1.58019549404244,-4.86334165753292,
-2.94375));
#309748=CARTESIAN_POINT('Ctrl Pts',(2.85860050315749,-3.93452605039576,
-2.85625));
#309749=CARTESIAN_POINT('Ctrl Pts',(4.13700551227253,-3.0057104432586,-2.76875));
#309750=CARTESIAN_POINT('Ctrl Pts',(4.62531277436636,-1.5028552216293,-2.68125));
#309751=CARTESIAN_POINT('Ctrl Pts',(5.11362003646019,7.95366714520796E-16,
-2.59375));
#309752=CARTESIAN_POINT('Ctrl Pts',(4.62531277436636,1.5028552216293,-2.50625));
#309753=CARTESIAN_POINT('Ctrl Pts',(4.13700551227253,3.0057104432586,-2.41875));
#309754=CARTESIAN_POINT('Ctrl Pts',(2.85860050315749,3.93452605039576,-2.33125));
#309755=CARTESIAN_POINT('Ctrl Pts',(1.58019549404244,4.86334165753292,-2.24375));
#309756=CARTESIAN_POINT('Ctrl Pts',(0.,4.86334165753293,-2.15625));
#309757=CARTESIAN_POINT('Ctrl Pts',(-1.58019549404244,4.86334165753292,
-2.06875));
#309758=CARTESIAN_POINT('Ctrl Pts',(-2.85860050315749,3.93452605039576,
-1.98125));
#309759=CARTESIAN_POINT('Ctrl Pts',(-4.13700551227253,3.0057104432586,-1.89375));
#309760=CARTESIAN_POINT('Ctrl Pts',(-4.62531277436636,1.5028552216293,-1.80625));
#309761=CARTESIAN_POINT('Ctrl Pts',(-5.11362003646019,2.04784239646214E-15,
-1.71875));
#309762=CARTESIAN_POINT('Ctrl Pts',(-4.62531277436636,-1.5028552216293,
-1.63125));
#309763=CARTESIAN_POINT('Ctrl Pts',(-4.13700551227253,-3.00571044325859,
-1.54375));
#309764=CARTESIAN_POINT('Ctrl Pts',(-2.85860050315749,-3.93452605039576,
-1.45625));
#309765=CARTESIAN_POINT('Ctrl Pts',(-1.58019549404244,-4.86334165753292,
-1.36875));
#309766=CARTESIAN_POINT('Ctrl Pts',(-5.95587579405768E-16,-4.86334165753292,
-1.28125));
#309767=CARTESIAN_POINT('',(5.61169055981797,-3.60964178854093E-16,-3.91169055981797));
#309768=CARTESIAN_POINT('Ctrl Pts',(-2.21250112451911,-4.33092725082016,
-3.16334165753291));
#309769=CARTESIAN_POINT('Ctrl Pts',(-2.60719450358133,-4.14710387972064,
-3.17920192465262));
#309770=CARTESIAN_POINT('Ctrl Pts',(-2.97433163955537,-3.91057564075788,
-3.19414831697094));
#309771=CARTESIAN_POINT('Ctrl Pts',(-3.6304946963471,-3.35510992093543,
-3.22490945247993));
#309772=CARTESIAN_POINT('Ctrl Pts',(-3.91956573332253,-3.03773926555733,
-3.24048010635175));
#309773=CARTESIAN_POINT('Ctrl Pts',(-4.5672278566538,-2.10952655564697,
-3.28138802246961));
#309774=CARTESIAN_POINT('Ctrl Pts',(-4.81509817539142,-1.49220678589881,
-3.30351920138978));
#309775=CARTESIAN_POINT('Ctrl Pts',(-5.08200700866935,-0.261756534382178,
-3.34775565193902));
#309776=CARTESIAN_POINT('Ctrl Pts',(-5.09681794441811,0.38892707590372,
-3.37082896809827));
#309777=CARTESIAN_POINT('Ctrl Pts',(-4.93227195395555,1.35860806500034,
-3.40476619169824));
#309778=CARTESIAN_POINT('Ctrl Pts',(-4.84196850476752,1.68543727529175,
-3.41591449154964));
#309779=CARTESIAN_POINT('Ctrl Pts',(-4.48337515897765,2.61986203920909,
-3.45003070344122));
#309780=CARTESIAN_POINT('Ctrl Pts',(-4.12755756215163,3.18876467727029,
-3.47333923889199));
#309781=CARTESIAN_POINT('Ctrl Pts',(-3.16576211569989,4.21826206367995,
-3.52138522726153));
#309782=CARTESIAN_POINT('Ctrl Pts',(-2.57933682320399,4.61137003710499,
-3.5437507450149));
#309783=CARTESIAN_POINT('Ctrl Pts',(-1.38321071187134,5.1468107907079,-3.5882824311065));
#309784=CARTESIAN_POINT('Ctrl Pts',(-0.734020794814275,5.3011330060117,
-3.61071457969699));
#309785=CARTESIAN_POINT('Ctrl Pts',(0.279946897817617,5.34769015241393,
-3.64334071581177));
#309786=CARTESIAN_POINT('Ctrl Pts',(0.636284073092541,5.32892781932006,
-3.65490827023087));
#309787=CARTESIAN_POINT('Ctrl Pts',(1.33403158204166,5.22189855460367,-3.67831196246797));
#309788=CARTESIAN_POINT('Ctrl Pts',(1.67297966356761,5.13560563080429,-3.68996111196863));
#309789=CARTESIAN_POINT('Ctrl Pts',(2.72455580662618,4.75605569057548,-3.72701605611379));
#309790=CARTESIAN_POINT('Ctrl Pts',(3.33392558335127,4.36173352953152,-3.74913968805936));
#309791=CARTESIAN_POINT('Ctrl Pts',(4.35401110494811,3.4259477650097,-3.79390141753689));
#309792=CARTESIAN_POINT('Ctrl Pts',(4.78185486937148,2.84385742230068,-3.81743010764088));
#309793=CARTESIAN_POINT('Ctrl Pts',(5.24058372029848,1.86746156353265,-3.8515209540203));
#309794=CARTESIAN_POINT('Ctrl Pts',(5.36179283297534,1.52406097865491,-3.86252927606252));
#309795=CARTESIAN_POINT('Ctrl Pts',(5.54463674231665,0.788760206188264,
-3.88637233212224));
#309796=CARTESIAN_POINT('Ctrl Pts',(5.59905017436476,0.395144997205665,
-3.89905017436476));
#309797=CARTESIAN_POINT('Ctrl Pts',(5.61169055981797,-9.0205620750794E-16,
-3.91169055981797));
#309798=CARTESIAN_POINT('Ctrl Pts',(5.61169055981797,-1.38777878078145E-16,
-3.91169055981797));
#309799=CARTESIAN_POINT('Ctrl Pts',(5.62208535815845,-0.324946780808796,
-3.92208535815844));
#309800=CARTESIAN_POINT('Ctrl Pts',(5.60423157167623,-0.650928060576569,
-3.93245506337904));
#309801=CARTESIAN_POINT('Ctrl Pts',(5.45274517051411,-1.70904678777463,
-3.96593365768693));
#309802=CARTESIAN_POINT('Ctrl Pts',(5.20163226652447,-2.41677199412078,
-3.98794350103121));
#309803=CARTESIAN_POINT('Ctrl Pts',(4.63717212063039,-3.37429620405354,
-4.02279179045299));
#309804=CARTESIAN_POINT('Ctrl Pts',(4.41686272435106,-3.67622261701962,
-4.03449108433516));
#309805=CARTESIAN_POINT('Ctrl Pts',(3.62352289881408,-4.56616302478096,
-4.07140204215783));
#309806=CARTESIAN_POINT('Ctrl Pts',(2.9915333438317,-5.01055071564082,-4.09348040363817));
#309807=CARTESIAN_POINT('Ctrl Pts',(1.66811522085473,-5.64761620972557,
-4.13855742806273));
#309808=CARTESIAN_POINT('Ctrl Pts',(0.916971204147396,-5.84075811028472,
-4.16223199641104));
#309809=CARTESIAN_POINT('Ctrl Pts',(-0.0143208385757574,-5.89177397945501,
-4.18949497944445));
#309810=CARTESIAN_POINT('Ctrl Pts',(-0.179394107925109,-5.89380659597007,
-4.19425881377196));
#309811=CARTESIAN_POINT('Ctrl Pts',(-0.904890135639625,-5.87291322183324,
-4.21561668306337));
#309812=CARTESIAN_POINT('Ctrl Pts',(-1.46138320786938,-5.77716446381248,
-4.23261174044124));
#309813=CARTESIAN_POINT('Ctrl Pts',(-2.2637783039818,-5.51837303963243,
-4.25802866316144));
#309814=CARTESIAN_POINT('Ctrl Pts',(-2.52498189660555,-5.41314737249321,
-4.26646170234364));
#309815=CARTESIAN_POINT('Ctrl Pts',(-3.03708821495135,-5.16328569590837,
-4.28332938416876));
#309816=CARTESIAN_POINT('Ctrl Pts',(-3.28525172634026,-5.01924798335745,
-4.29167943232946));
#309817=CARTESIAN_POINT('Ctrl Pts',(-3.52671151375647,-4.85410196624857,
-4.30000000000005));
#309818=CARTESIAN_POINT('Origin',(2.99770677028732E-14,-1.99840144432528E-14,
-5.765625));
#309819=CARTESIAN_POINT('',(1.48910022457091,-4.62975945369497,-3.16334165753294));
#309820=CARTESIAN_POINT('Ctrl Pts',(1.48910022457091,-4.62975945369497,
-3.16334165753294));
#309821=CARTESIAN_POINT('Ctrl Pts',(2.22943715735947,-4.39163997818016,
-3.11806287316211));
#309822=CARTESIAN_POINT('Ctrl Pts',(2.85860050315749,-3.93452605039576,
-3.075));
#309823=CARTESIAN_POINT('Ctrl Pts',(4.13700551227253,-3.0057104432586,-2.9875));
#309824=CARTESIAN_POINT('Ctrl Pts',(4.62531277436636,-1.5028552216293,-2.9));
#309825=CARTESIAN_POINT('Ctrl Pts',(5.11362003646019,7.95366714520796E-16,
-2.8125));
#309826=CARTESIAN_POINT('Ctrl Pts',(4.62531277436636,1.5028552216293,-2.725));
#309827=CARTESIAN_POINT('Ctrl Pts',(4.13700551227253,3.0057104432586,-2.6375));
#309828=CARTESIAN_POINT('Ctrl Pts',(2.85860050315749,3.93452605039576,-2.55));
#309829=CARTESIAN_POINT('Ctrl Pts',(1.58019549404244,4.86334165753292,-2.4625));
#309830=CARTESIAN_POINT('Ctrl Pts',(0.,4.86334165753293,-2.375));
#309831=CARTESIAN_POINT('Ctrl Pts',(-1.58019549404244,4.86334165753292,
-2.2875));
#309832=CARTESIAN_POINT('Ctrl Pts',(-2.85860050315749,3.93452605039576,
-2.2));
#309833=CARTESIAN_POINT('Ctrl Pts',(-4.13700551227253,3.0057104432586,-2.1125));
#309834=CARTESIAN_POINT('Ctrl Pts',(-4.62531277436636,1.5028552216293,-2.025));
#309835=CARTESIAN_POINT('Ctrl Pts',(-5.11362003646019,2.04784239646214E-15,
-1.9375));
#309836=CARTESIAN_POINT('Ctrl Pts',(-4.62531277436636,-1.5028552216293,
-1.85));
#309837=CARTESIAN_POINT('Ctrl Pts',(-4.13700551227253,-3.00571044325859,
-1.7625));
#309838=CARTESIAN_POINT('Ctrl Pts',(-2.85860050315749,-3.93452605039576,
-1.675));
#309839=CARTESIAN_POINT('Ctrl Pts',(-1.58019549404244,-4.86334165753292,
-1.5875));
#309840=CARTESIAN_POINT('Ctrl Pts',(-5.95587579405768E-16,-4.86334165753292,
-1.5));
#309841=CARTESIAN_POINT('Origin',(2.99770677028732E-14,-1.99840144432528E-14,
-3.16334165753295));
#309842=CARTESIAN_POINT('Ctrl Pts',(0.,4.86333489545091,-5.87499609591012));
#309843=CARTESIAN_POINT('Ctrl Pts',(-1.5801932969088,4.8633348954509,-5.78749609591012));
#309844=CARTESIAN_POINT('Ctrl Pts',(-2.8585965285054,3.93452057975648,-5.69999609591012));
#309845=CARTESIAN_POINT('Ctrl Pts',(-4.13699976010199,3.00570626406207,
-5.61249609591012));
#309846=CARTESIAN_POINT('Ctrl Pts',(-4.62530634324419,1.50285313203104,
-5.52499609591012));
#309847=CARTESIAN_POINT('Ctrl Pts',(-5.11361292638638,2.04784196109569E-15,
-5.43749609591012));
#309848=CARTESIAN_POINT('Ctrl Pts',(-4.62530634324419,-1.50285313203103,
-5.34999609591012));
#309849=CARTESIAN_POINT('Ctrl Pts',(-4.13699976010199,-3.00570626406207,
-5.26249609591011));
#309850=CARTESIAN_POINT('Ctrl Pts',(-2.8585965285054,-3.93452057975648,
-5.17499609591012));
#309851=CARTESIAN_POINT('Ctrl Pts',(-1.5801932969088,-4.8633348954509,-5.08749609591013));
#309852=CARTESIAN_POINT('Ctrl Pts',(-5.95586751289557E-16,-4.8633348954509,
-4.99999609591012));
#309853=CARTESIAN_POINT('Ctrl Pts',(1.5801932969088,-4.8633348954509,-4.91249609591012));
#309854=CARTESIAN_POINT('Ctrl Pts',(2.8585965285054,-3.93452057975648,-4.82499609591012));
#309855=CARTESIAN_POINT('Ctrl Pts',(4.13699976010199,-3.00570626406207,
-4.73749609591012));
#309856=CARTESIAN_POINT('Ctrl Pts',(4.62530634324419,-1.50285313203104,
-4.64999609591012));
#309857=CARTESIAN_POINT('Ctrl Pts',(5.11361292638638,7.95368020620165E-16,
-4.56249609591012));
#309858=CARTESIAN_POINT('Ctrl Pts',(4.62530634324419,1.50285313203104,-4.47499609591012));
#309859=CARTESIAN_POINT('Ctrl Pts',(4.13699976010199,3.00570626406207,-4.38749609591012));
#309860=CARTESIAN_POINT('Ctrl Pts',(2.8585965285054,3.93452057975648,-4.29999609591012));
#309861=CARTESIAN_POINT('Ctrl Pts',(1.5801932969088,4.8633348954509,-4.21249609591012));
#309862=CARTESIAN_POINT('Ctrl Pts',(0.,4.86333489545091,-4.12499609591012));
#309863=CARTESIAN_POINT('Ctrl Pts',(-1.5801932969088,4.8633348954509,-4.03749609591012));
#309864=CARTESIAN_POINT('Ctrl Pts',(-2.8585965285054,3.93452057975648,-3.94999609591012));
#309865=CARTESIAN_POINT('Ctrl Pts',(-4.13699976010199,3.00570626406207,
-3.86249609591012));
#309866=CARTESIAN_POINT('Ctrl Pts',(-4.62530634324419,1.50285313203104,
-3.77499609591012));
#309867=CARTESIAN_POINT('Ctrl Pts',(-5.11361292638638,2.04784196109569E-15,
-3.68749609591012));
#309868=CARTESIAN_POINT('Ctrl Pts',(-4.62530634324419,-1.50285313203103,
-3.59999609591012));
#309869=CARTESIAN_POINT('Ctrl Pts',(-4.13699976010199,-3.00570626406207,
-3.51249609591012));
#309870=CARTESIAN_POINT('Ctrl Pts',(-2.8585965285054,-3.93452057975648,
-3.42499609591012));
#309871=CARTESIAN_POINT('Ctrl Pts',(-1.5801932969088,-4.8633348954509,-3.33749609591012));
#309872=CARTESIAN_POINT('Ctrl Pts',(-5.95586751289557E-16,-4.8633348954509,
-3.24999609591012));
#309873=CARTESIAN_POINT('Ctrl Pts',(1.5801932969088,-4.8633348954509,-3.16249609591012));
#309874=CARTESIAN_POINT('Ctrl Pts',(2.8585965285054,-3.93452057975648,-3.07499609591012));
#309875=CARTESIAN_POINT('Ctrl Pts',(4.13699976010199,-3.00570626406207,
-2.98749609591012));
#309876=CARTESIAN_POINT('Ctrl Pts',(4.62530634324419,-1.50285313203104,
-2.89999609591012));
#309877=CARTESIAN_POINT('Ctrl Pts',(5.11361292638638,7.95368020620165E-16,
-2.81249609591012));
#309878=CARTESIAN_POINT('Ctrl Pts',(4.62530634324419,1.50285313203104,-2.72499609591012));
#309879=CARTESIAN_POINT('Ctrl Pts',(4.13699976010199,3.00570626406207,-2.63749609591012));
#309880=CARTESIAN_POINT('Ctrl Pts',(2.8585965285054,3.93452057975648,-2.54999609591012));
#309881=CARTESIAN_POINT('Ctrl Pts',(1.5801932969088,4.8633348954509,-2.46249609591012));
#309882=CARTESIAN_POINT('Ctrl Pts',(0.,4.86333489545091,-2.37499609591012));
#309883=CARTESIAN_POINT('Ctrl Pts',(-1.5801932969088,4.8633348954509,-2.28749609591012));
#309884=CARTESIAN_POINT('Ctrl Pts',(-2.8585965285054,3.93452057975648,-2.19999609591012));
#309885=CARTESIAN_POINT('Ctrl Pts',(-4.13699976010199,3.00570626406207,
-2.11249609591012));
#309886=CARTESIAN_POINT('Ctrl Pts',(-4.62530634324419,1.50285313203104,
-2.02499609591012));
#309887=CARTESIAN_POINT('Ctrl Pts',(-5.11361292638638,2.04784196109569E-15,
-1.93749609591012));
#309888=CARTESIAN_POINT('Ctrl Pts',(-4.62530634324419,-1.50285313203103,
-1.84999609591012));
#309889=CARTESIAN_POINT('Ctrl Pts',(-4.13699976010199,-3.00570626406207,
-1.76249609591012));
#309890=CARTESIAN_POINT('Ctrl Pts',(-2.8585965285054,-3.93452057975648,
-1.67499609591012));
#309891=CARTESIAN_POINT('Ctrl Pts',(-1.5801932969088,-4.8633348954509,-1.58749609591012));
#309892=CARTESIAN_POINT('Ctrl Pts',(-5.95586751289557E-16,-4.8633348954509,
-1.49999609591012));
#309893=CARTESIAN_POINT('Ctrl Pts',(1.5801932969088,-4.8633348954509,-1.41249609591012));
#309894=CARTESIAN_POINT('Ctrl Pts',(2.8585965285054,-3.93452057975648,-1.32499609591012));
#309895=CARTESIAN_POINT('Ctrl Pts',(4.13699976010199,-3.00570626406207,
-1.23749609591012));
#309896=CARTESIAN_POINT('Ctrl Pts',(4.62530634324419,-1.50285313203104,
-1.14999609591012));
#309897=CARTESIAN_POINT('Ctrl Pts',(5.11361292638638,7.95368020620165E-16,
-1.06249609591012));
#309898=CARTESIAN_POINT('Ctrl Pts',(4.62530634324419,1.50285313203104,-0.974996095910122));
#309899=CARTESIAN_POINT('Ctrl Pts',(4.13699976010199,3.00570626406207,-0.887496095910121));
#309900=CARTESIAN_POINT('Ctrl Pts',(2.8585965285054,3.93452057975648,-0.799996095910123));
#309901=CARTESIAN_POINT('Ctrl Pts',(1.5801932969088,4.8633348954509,-0.712496095910121));
#309902=CARTESIAN_POINT('Ctrl Pts',(0.,4.86333489545091,-0.624996095910122));
#309903=CARTESIAN_POINT('Ctrl Pts',(-1.5801932969088,4.8633348954509,-0.537496095910121));
#309904=CARTESIAN_POINT('Ctrl Pts',(-2.8585965285054,3.93452057975648,-0.449996095910122));
#309905=CARTESIAN_POINT('Ctrl Pts',(-4.13699976010199,3.00570626406207,
-0.362496095910121));
#309906=CARTESIAN_POINT('Ctrl Pts',(-4.62530634324419,1.50285313203104,
-0.274996095910122));
#309907=CARTESIAN_POINT('Ctrl Pts',(-5.11361292638638,2.04784196109569E-15,
-0.187496095910121));
#309908=CARTESIAN_POINT('Ctrl Pts',(-4.62530634324419,-1.50285313203103,
-0.0999960959101223));
#309909=CARTESIAN_POINT('Ctrl Pts',(-4.13699976010199,-3.00570626406207,
-0.0124960959101217));
#309910=CARTESIAN_POINT('Ctrl Pts',(-2.8585965285054,-3.93452057975648,
0.0750039040898777));
#309911=CARTESIAN_POINT('Ctrl Pts',(-1.5801932969088,-4.8633348954509,0.162503904089879));
#309912=CARTESIAN_POINT('Ctrl Pts',(-5.95586751289557E-16,-4.8633348954509,
0.250003904089878));
#309913=CARTESIAN_POINT('Ctrl Pts',(1.5801932969088,-4.8633348954509,0.337503904089879));
#309914=CARTESIAN_POINT('Ctrl Pts',(2.8585965285054,-3.93452057975648,0.425003904089878));
#309915=CARTESIAN_POINT('Ctrl Pts',(4.13699976010199,-3.00570626406207,
0.512503904089878));
#309916=CARTESIAN_POINT('Ctrl Pts',(4.62530634324419,-1.50285313203104,
0.600003904089878));
#309917=CARTESIAN_POINT('Ctrl Pts',(5.11361292638638,7.95368020620165E-16,
0.687503904089878));
#309918=CARTESIAN_POINT('Ctrl Pts',(4.62530634324419,1.50285313203104,0.775003904089878));
#309919=CARTESIAN_POINT('Ctrl Pts',(4.13699976010199,3.00570626406207,0.862503904089877));
#309920=CARTESIAN_POINT('Ctrl Pts',(2.8585965285054,3.93452057975648,0.950003904089878));
#309921=CARTESIAN_POINT('Ctrl Pts',(1.5801932969088,4.8633348954509,1.03750390408988));
#309922=CARTESIAN_POINT('Ctrl Pts',(0.,4.86333489545091,1.12500390408988));
#309923=CARTESIAN_POINT('Ctrl Pts',(-1.5801932969088,4.8633348954509,1.21250390408988));
#309924=CARTESIAN_POINT('Ctrl Pts',(-2.8585965285054,3.93452057975648,1.30000390408988));
#309925=CARTESIAN_POINT('Ctrl Pts',(-4.13699976010199,3.00570626406207,
1.38750390408988));
#309926=CARTESIAN_POINT('Ctrl Pts',(-4.62530634324419,1.50285313203104,
1.47500390408988));
#309927=CARTESIAN_POINT('Ctrl Pts',(-5.11361292638638,2.04784196109569E-15,
1.56250390408988));
#309928=CARTESIAN_POINT('Ctrl Pts',(-4.62530634324419,-1.50285313203103,
1.65000390408988));
#309929=CARTESIAN_POINT('Ctrl Pts',(-4.13699976010199,-3.00570626406207,
1.73750390408988));
#309930=CARTESIAN_POINT('Ctrl Pts',(-2.8585965285054,-3.93452057975648,
1.82500390408988));
#309931=CARTESIAN_POINT('Ctrl Pts',(-1.5801932969088,-4.8633348954509,1.91250390408988));
#309932=CARTESIAN_POINT('Ctrl Pts',(-5.95586751289557E-16,-4.8633348954509,
2.00000390408988));
#309933=CARTESIAN_POINT('Ctrl Pts',(1.5801932969088,-4.8633348954509,2.08750390408988));
#309934=CARTESIAN_POINT('Ctrl Pts',(2.8585965285054,-3.93452057975648,2.17500390408988));
#309935=CARTESIAN_POINT('Ctrl Pts',(4.13699976010199,-3.00570626406207,
2.26250390408988));
#309936=CARTESIAN_POINT('Ctrl Pts',(4.62530634324419,-1.50285313203104,
2.35000390408988));
#309937=CARTESIAN_POINT('Ctrl Pts',(5.11361292638638,7.95368020620165E-16,
2.43750390408988));
#309938=CARTESIAN_POINT('Ctrl Pts',(4.62530634324419,1.50285313203104,2.52500390408988));
#309939=CARTESIAN_POINT('Ctrl Pts',(4.13699976010199,3.00570626406207,2.61250390408988));
#309940=CARTESIAN_POINT('Ctrl Pts',(2.8585965285054,3.93452057975648,2.70000390408988));
#309941=CARTESIAN_POINT('Ctrl Pts',(1.5801932969088,4.8633348954509,2.78750390408988));
#309942=CARTESIAN_POINT('Ctrl Pts',(0.,4.86333489545091,2.87500390408988));
#309943=CARTESIAN_POINT('Ctrl Pts',(-1.5801932969088,4.8633348954509,2.96250390408988));
#309944=CARTESIAN_POINT('Ctrl Pts',(-2.8585965285054,3.93452057975648,3.05000390408988));
#309945=CARTESIAN_POINT('Ctrl Pts',(-4.13699976010199,3.00570626406207,
3.13750390408988));
#309946=CARTESIAN_POINT('Ctrl Pts',(-4.62530634324419,1.50285313203104,
3.22500390408988));
#309947=CARTESIAN_POINT('Ctrl Pts',(-5.11361292638638,2.04784196109569E-15,
3.31250390408987));
#309948=CARTESIAN_POINT('Ctrl Pts',(-4.62530634324419,-1.50285313203103,
3.40000390408988));
#309949=CARTESIAN_POINT('Ctrl Pts',(-4.13699976010199,-3.00570626406207,
3.48750390408988));
#309950=CARTESIAN_POINT('Ctrl Pts',(-2.8585965285054,-3.93452057975648,
3.57500390408988));
#309951=CARTESIAN_POINT('Ctrl Pts',(-1.5801932969088,-4.8633348954509,3.66250390408988));
#309952=CARTESIAN_POINT('Ctrl Pts',(-5.95586751289557E-16,-4.8633348954509,
3.75000390408988));
#309953=CARTESIAN_POINT('Ctrl Pts',(1.5801932969088,-4.8633348954509,3.83750390408988));
#309954=CARTESIAN_POINT('Ctrl Pts',(2.8585965285054,-3.93452057975648,3.92500390408988));
#309955=CARTESIAN_POINT('Ctrl Pts',(4.13699976010199,-3.00570626406207,
4.01250390408988));
#309956=CARTESIAN_POINT('Ctrl Pts',(4.62530634324419,-1.50285313203104,
4.10000390408988));
#309957=CARTESIAN_POINT('Ctrl Pts',(5.11361292638638,7.95368020620165E-16,
4.18750390408988));
#309958=CARTESIAN_POINT('Ctrl Pts',(4.62530634324419,1.50285313203104,4.27500390408988));
#309959=CARTESIAN_POINT('Ctrl Pts',(4.13699976010199,3.00570626406207,4.36250390408988));
#309960=CARTESIAN_POINT('Ctrl Pts',(2.8585965285054,3.93452057975648,4.45000390408988));
#309961=CARTESIAN_POINT('Ctrl Pts',(1.5801932969088,4.8633348954509,4.53750390408988));
#309962=CARTESIAN_POINT('Ctrl Pts',(0.,4.86333489545091,4.62500390408988));
#309963=CARTESIAN_POINT('Ctrl Pts',(-1.5801932969088,4.8633348954509,4.71250390408988));
#309964=CARTESIAN_POINT('Ctrl Pts',(-2.8585965285054,3.93452057975648,4.80000390408988));
#309965=CARTESIAN_POINT('Ctrl Pts',(-4.13699976010199,3.00570626406207,
4.88750390408987));
#309966=CARTESIAN_POINT('Ctrl Pts',(-4.62530634324419,1.50285313203104,
4.97500390408988));
#309967=CARTESIAN_POINT('Ctrl Pts',(-5.11361292638638,2.04784196109569E-15,
5.06250390408988));
#309968=CARTESIAN_POINT('Ctrl Pts',(-4.62530634324419,-1.50285313203103,
5.15000390408988));
#309969=CARTESIAN_POINT('Ctrl Pts',(-4.13699976010199,-3.00570626406207,
5.23750390408988));
#309970=CARTESIAN_POINT('Ctrl Pts',(-2.8585965285054,-3.93452057975648,
5.32500390408988));
#309971=CARTESIAN_POINT('Ctrl Pts',(-1.5801932969088,-4.8633348954509,5.41250390408988));
#309972=CARTESIAN_POINT('Ctrl Pts',(-5.95586751289557E-16,-4.8633348954509,
5.50000390408988));
#309973=CARTESIAN_POINT('Ctrl Pts',(1.5801932969088,-4.8633348954509,5.58750390408987));
#309974=CARTESIAN_POINT('Ctrl Pts',(2.8585965285054,-3.93452057975648,5.67500390408988));
#309975=CARTESIAN_POINT('Ctrl Pts',(4.13699976010199,-3.00570626406207,
5.76250390408987));
#309976=CARTESIAN_POINT('Ctrl Pts',(4.62530634324419,-1.50285313203104,
5.85000390408988));
#309977=CARTESIAN_POINT('Ctrl Pts',(4.69280400630547,-1.29511668562952,
5.86209885779675));
#309978=CARTESIAN_POINT('Ctrl Pts',(4.74140733325457,-1.08216579389214,
5.87449741001046));
#309979=CARTESIAN_POINT('Ctrl Pts',(0.,6.09472152853892,-6.5859375));
#309980=CARTESIAN_POINT('Ctrl Pts',(-1.98029506767702,6.09472152853892,
-6.4984375));
#309981=CARTESIAN_POINT('Ctrl Pts',(-3.58238743130461,4.93073329257085,
-6.4109375));
#309982=CARTESIAN_POINT('Ctrl Pts',(-5.18447979493221,3.76674505660277,
-6.3234375));
#309983=CARTESIAN_POINT('Ctrl Pts',(-5.7964246247213,1.88337252830138,-6.2359375));
#309984=CARTESIAN_POINT('Ctrl Pts',(-6.40836945451038,2.1271229329878E-15,
-6.14843749999999));
#309985=CARTESIAN_POINT('Ctrl Pts',(-5.7964246247213,-1.88337252830138,
-6.0609375));
#309986=CARTESIAN_POINT('Ctrl Pts',(-5.18447979493221,-3.76674505660276,
-5.9734375));
#309987=CARTESIAN_POINT('Ctrl Pts',(-3.58238743130461,-4.93073329257084,
-5.8859375));
#309988=CARTESIAN_POINT('Ctrl Pts',(-1.98029506767702,-6.09472152853892,
-5.7984375));
#309989=CARTESIAN_POINT('Ctrl Pts',(-7.46388121161965E-16,-6.09472152853892,
-5.7109375));
#309990=CARTESIAN_POINT('Ctrl Pts',(1.98029506767702,-6.09472152853892,
-5.6234375));
#309991=CARTESIAN_POINT('Ctrl Pts',(3.58238743130461,-4.93073329257084,
-5.5359375));
#309992=CARTESIAN_POINT('Ctrl Pts',(5.18447979493221,-3.76674505660276,
-5.44843749999999));
#309993=CARTESIAN_POINT('Ctrl Pts',(5.7964246247213,-1.88337252830138,-5.3609375));
#309994=CARTESIAN_POINT('Ctrl Pts',(6.40836945451038,5.57525104943835E-16,
-5.27343749999999));
#309995=CARTESIAN_POINT('Ctrl Pts',(5.7964246247213,1.88337252830138,-5.1859375));
#309996=CARTESIAN_POINT('Ctrl Pts',(5.18447979493221,3.76674505660277,-5.09843749999999));
#309997=CARTESIAN_POINT('Ctrl Pts',(3.58238743130462,4.93073329257084,-5.0109375));
#309998=CARTESIAN_POINT('Ctrl Pts',(1.98029506767702,6.09472152853892,-4.9234375));
#309999=CARTESIAN_POINT('Ctrl Pts',(0.,6.09472152853892,-4.8359375));
#310000=CARTESIAN_POINT('Ctrl Pts',(-1.98029506767702,6.09472152853892,
-4.7484375));
#310001=CARTESIAN_POINT('Ctrl Pts',(-3.58238743130461,4.93073329257085,
-4.6609375));
#310002=CARTESIAN_POINT('Ctrl Pts',(-5.18447979493221,3.76674505660277,
-4.5734375));
#310003=CARTESIAN_POINT('Ctrl Pts',(-5.7964246247213,1.88337252830138,-4.4859375));
#310004=CARTESIAN_POINT('Ctrl Pts',(-6.40836945451038,2.1271229329878E-15,
-4.39843749999999));
#310005=CARTESIAN_POINT('Ctrl Pts',(-5.7964246247213,-1.88337252830138,
-4.3109375));
#310006=CARTESIAN_POINT('Ctrl Pts',(-5.18447979493221,-3.76674505660276,
-4.2234375));
#310007=CARTESIAN_POINT('Ctrl Pts',(-3.58238743130461,-4.93073329257084,
-4.1359375));
#310008=CARTESIAN_POINT('Ctrl Pts',(-1.98029506767702,-6.09472152853892,
-4.0484375));
#310009=CARTESIAN_POINT('Ctrl Pts',(-7.46388121161965E-16,-6.09472152853892,
-3.96093749999999));
#310010=CARTESIAN_POINT('Ctrl Pts',(1.98029506767702,-6.09472152853892,
-3.87343749999999));
#310011=CARTESIAN_POINT('Ctrl Pts',(3.58238743130461,-4.93073329257084,
-3.7859375));
#310012=CARTESIAN_POINT('Ctrl Pts',(5.18447979493221,-3.76674505660276,
-3.6984375));
#310013=CARTESIAN_POINT('Ctrl Pts',(5.7964246247213,-1.88337252830138,-3.6109375));
#310014=CARTESIAN_POINT('Ctrl Pts',(6.40836945451038,5.57525104943835E-16,
-3.5234375));
#310015=CARTESIAN_POINT('Ctrl Pts',(5.7964246247213,1.88337252830138,-3.4359375));
#310016=CARTESIAN_POINT('Ctrl Pts',(5.18447979493221,3.76674505660277,-3.34843749999999));
#310017=CARTESIAN_POINT('Ctrl Pts',(3.58238743130462,4.93073329257084,-3.2609375));
#310018=CARTESIAN_POINT('Ctrl Pts',(1.98029506767702,6.09472152853892,-3.1734375));
#310019=CARTESIAN_POINT('Ctrl Pts',(0.,6.09472152853892,-3.0859375));
#310020=CARTESIAN_POINT('Ctrl Pts',(-1.98029506767702,6.09472152853892,
-2.9984375));
#310021=CARTESIAN_POINT('Ctrl Pts',(-3.58238743130461,4.93073329257085,
-2.9109375));
#310022=CARTESIAN_POINT('Ctrl Pts',(-5.18447979493221,3.76674505660277,
-2.8234375));
#310023=CARTESIAN_POINT('Ctrl Pts',(-5.7964246247213,1.88337252830138,-2.7359375));
#310024=CARTESIAN_POINT('Ctrl Pts',(-6.40836945451038,2.1271229329878E-15,
-2.6484375));
#310025=CARTESIAN_POINT('Ctrl Pts',(-5.7964246247213,-1.88337252830138,
-2.5609375));
#310026=CARTESIAN_POINT('Ctrl Pts',(-5.18447979493221,-3.76674505660276,
-2.4734375));
#310027=CARTESIAN_POINT('Ctrl Pts',(-3.58238743130461,-4.93073329257084,
-2.3859375));
#310028=CARTESIAN_POINT('Ctrl Pts',(-1.98029506767702,-6.09472152853892,
-2.2984375));
#310029=CARTESIAN_POINT('Ctrl Pts',(-7.46388121161965E-16,-6.09472152853892,
-2.2109375));
#310030=CARTESIAN_POINT('Ctrl Pts',(1.98029506767702,-6.09472152853892,
-2.12343749999999));
#310031=CARTESIAN_POINT('Ctrl Pts',(3.58238743130461,-4.93073329257084,
-2.0359375));
#310032=CARTESIAN_POINT('Ctrl Pts',(5.18447979493221,-3.76674505660276,
-1.9484375));
#310033=CARTESIAN_POINT('Ctrl Pts',(5.7964246247213,-1.88337252830138,-1.8609375));
#310034=CARTESIAN_POINT('Ctrl Pts',(6.40836945451038,5.57525104943835E-16,
-1.7734375));
#310035=CARTESIAN_POINT('Ctrl Pts',(5.7964246247213,1.88337252830138,-1.6859375));
#310036=CARTESIAN_POINT('Ctrl Pts',(5.18447979493221,3.76674505660277,-1.5984375));
#310037=CARTESIAN_POINT('Ctrl Pts',(3.58238743130462,4.93073329257084,-1.5109375));
#310038=CARTESIAN_POINT('Ctrl Pts',(1.98029506767702,6.09472152853892,-1.4234375));
#310039=CARTESIAN_POINT('Ctrl Pts',(0.,6.09472152853892,-1.3359375));
#310040=CARTESIAN_POINT('Ctrl Pts',(-1.98029506767702,6.09472152853892,
-1.2484375));
#310041=CARTESIAN_POINT('Ctrl Pts',(-3.58238743130461,4.93073329257085,
-1.1609375));
#310042=CARTESIAN_POINT('Ctrl Pts',(-5.18447979493221,3.76674505660277,
-1.0734375));
#310043=CARTESIAN_POINT('Ctrl Pts',(-5.7964246247213,1.88337252830138,-0.9859375));
#310044=CARTESIAN_POINT('Ctrl Pts',(-6.40836945451038,2.1271229329878E-15,
-0.898437499999998));
#310045=CARTESIAN_POINT('Ctrl Pts',(-5.7964246247213,-1.88337252830138,
-0.8109375));
#310046=CARTESIAN_POINT('Ctrl Pts',(-5.18447979493221,-3.76674505660276,
-0.723437499999998));
#310047=CARTESIAN_POINT('Ctrl Pts',(-3.58238743130461,-4.93073329257084,
-0.6359375));
#310048=CARTESIAN_POINT('Ctrl Pts',(-1.98029506767702,-6.09472152853892,
-0.548437499999997));
#310049=CARTESIAN_POINT('Ctrl Pts',(-7.46388121161965E-16,-6.09472152853892,
-0.4609375));
#310050=CARTESIAN_POINT('Ctrl Pts',(1.98029506767702,-6.09472152853892,
-0.373437499999998));
#310051=CARTESIAN_POINT('Ctrl Pts',(3.58238743130461,-4.93073329257084,
-0.2859375));
#310052=CARTESIAN_POINT('Ctrl Pts',(5.18447979493221,-3.76674505660276,
-0.198437499999998));
#310053=CARTESIAN_POINT('Ctrl Pts',(5.7964246247213,-1.88337252830138,-0.110937499999998));
#310054=CARTESIAN_POINT('Ctrl Pts',(6.40836945451038,5.57525104943835E-16,
-0.0234374999999983));
#310055=CARTESIAN_POINT('Ctrl Pts',(5.7964246247213,1.88337252830138,0.0640625000000016));
#310056=CARTESIAN_POINT('Ctrl Pts',(5.18447979493221,3.76674505660277,0.151562500000001));
#310057=CARTESIAN_POINT('Ctrl Pts',(3.58238743130462,4.93073329257084,0.239062500000003));
#310058=CARTESIAN_POINT('Ctrl Pts',(1.98029506767702,6.09472152853892,0.326562500000002));
#310059=CARTESIAN_POINT('Ctrl Pts',(0.,6.09472152853892,0.4140625));
#310060=CARTESIAN_POINT('Ctrl Pts',(-1.98029506767702,6.09472152853892,
0.501562500000002));
#310061=CARTESIAN_POINT('Ctrl Pts',(-3.58238743130461,4.93073329257085,
0.5890625));
#310062=CARTESIAN_POINT('Ctrl Pts',(-5.18447979493221,3.76674505660277,
0.676562500000002));
#310063=CARTESIAN_POINT('Ctrl Pts',(-5.7964246247213,1.88337252830138,0.7640625));
#310064=CARTESIAN_POINT('Ctrl Pts',(-6.40836945451038,2.1271229329878E-15,
0.851562500000001));
#310065=CARTESIAN_POINT('Ctrl Pts',(-5.7964246247213,-1.88337252830138,
0.9390625));
#310066=CARTESIAN_POINT('Ctrl Pts',(-5.18447979493221,-3.76674505660276,
1.0265625));
#310067=CARTESIAN_POINT('Ctrl Pts',(-3.58238743130461,-4.93073329257084,
1.1140625));
#310068=CARTESIAN_POINT('Ctrl Pts',(-1.98029506767702,-6.09472152853892,
1.2015625));
#310069=CARTESIAN_POINT('Ctrl Pts',(-7.46388121161965E-16,-6.09472152853892,
1.2890625));
#310070=CARTESIAN_POINT('Ctrl Pts',(1.98029506767702,-6.09472152853892,
1.3765625));
#310071=CARTESIAN_POINT('Ctrl Pts',(3.58238743130461,-4.93073329257084,
1.4640625));
#310072=CARTESIAN_POINT('Ctrl Pts',(5.18447979493221,-3.76674505660276,
1.5515625));
#310073=CARTESIAN_POINT('Ctrl Pts',(5.7964246247213,-1.88337252830138,1.6390625));
#310074=CARTESIAN_POINT('Ctrl Pts',(6.40836945451038,5.57525104943835E-16,
1.7265625));
#310075=CARTESIAN_POINT('Ctrl Pts',(5.7964246247213,1.88337252830138,1.8140625));
#310076=CARTESIAN_POINT('Ctrl Pts',(5.18447979493221,3.76674505660277,1.9015625));
#310077=CARTESIAN_POINT('Ctrl Pts',(3.58238743130462,4.93073329257084,1.9890625));
#310078=CARTESIAN_POINT('Ctrl Pts',(1.98029506767702,6.09472152853892,2.0765625));
#310079=CARTESIAN_POINT('Ctrl Pts',(0.,6.09472152853892,2.1640625));
#310080=CARTESIAN_POINT('Ctrl Pts',(-1.98029506767702,6.09472152853892,
2.2515625));
#310081=CARTESIAN_POINT('Ctrl Pts',(-3.58238743130461,4.93073329257085,
2.33906250000001));
#310082=CARTESIAN_POINT('Ctrl Pts',(-5.18447979493221,3.76674505660277,
2.4265625));
#310083=CARTESIAN_POINT('Ctrl Pts',(-5.7964246247213,1.88337252830138,2.5140625));
#310084=CARTESIAN_POINT('Ctrl Pts',(-6.40836945451038,2.1271229329878E-15,
2.6015625));
#310085=CARTESIAN_POINT('Ctrl Pts',(-5.7964246247213,-1.88337252830138,
2.6890625));
#310086=CARTESIAN_POINT('Ctrl Pts',(-5.18447979493221,-3.76674505660276,
2.7765625));
#310087=CARTESIAN_POINT('Ctrl Pts',(-3.58238743130461,-4.93073329257084,
2.8640625));
#310088=CARTESIAN_POINT('Ctrl Pts',(-1.98029506767702,-6.09472152853892,
2.9515625));
#310089=CARTESIAN_POINT('Ctrl Pts',(-7.46388121161965E-16,-6.09472152853892,
3.0390625));
#310090=CARTESIAN_POINT('Ctrl Pts',(1.98029506767702,-6.09472152853892,
3.1265625));
#310091=CARTESIAN_POINT('Ctrl Pts',(3.58238743130461,-4.93073329257084,
3.2140625));
#310092=CARTESIAN_POINT('Ctrl Pts',(5.18447979493221,-3.76674505660276,
3.3015625));
#310093=CARTESIAN_POINT('Ctrl Pts',(5.7964246247213,-1.88337252830138,3.3890625));
#310094=CARTESIAN_POINT('Ctrl Pts',(6.40836945451038,5.57525104943835E-16,
3.4765625));
#310095=CARTESIAN_POINT('Ctrl Pts',(5.7964246247213,1.88337252830138,3.5640625));
#310096=CARTESIAN_POINT('Ctrl Pts',(5.18447979493221,3.76674505660277,3.6515625));
#310097=CARTESIAN_POINT('Ctrl Pts',(3.58238743130462,4.93073329257084,3.7390625));
#310098=CARTESIAN_POINT('Ctrl Pts',(1.98029506767702,6.09472152853892,3.8265625));
#310099=CARTESIAN_POINT('Ctrl Pts',(0.,6.09472152853892,3.91406250000001));
#310100=CARTESIAN_POINT('Ctrl Pts',(-1.98029506767702,6.09472152853892,
4.0015625));
#310101=CARTESIAN_POINT('Ctrl Pts',(-3.58238743130461,4.93073329257085,
4.0890625));
#310102=CARTESIAN_POINT('Ctrl Pts',(-5.18447979493221,3.76674505660277,
4.1765625));
#310103=CARTESIAN_POINT('Ctrl Pts',(-5.7964246247213,1.88337252830138,4.2640625));
#310104=CARTESIAN_POINT('Ctrl Pts',(-6.40836945451038,2.1271229329878E-15,
4.3515625));
#310105=CARTESIAN_POINT('Ctrl Pts',(-5.7964246247213,-1.88337252830138,
4.4390625));
#310106=CARTESIAN_POINT('Ctrl Pts',(-5.18447979493221,-3.76674505660276,
4.5265625));
#310107=CARTESIAN_POINT('Ctrl Pts',(-3.58238743130461,-4.93073329257084,
4.6140625));
#310108=CARTESIAN_POINT('Ctrl Pts',(-1.98029506767702,-6.09472152853892,
4.7015625));
#310109=CARTESIAN_POINT('Ctrl Pts',(-7.46388121161965E-16,-6.09472152853892,
4.7890625));
#310110=CARTESIAN_POINT('Ctrl Pts',(1.98029506767702,-6.09472152853892,
4.8765625));
#310111=CARTESIAN_POINT('Ctrl Pts',(3.58238743130461,-4.93073329257084,
4.9640625));
#310112=CARTESIAN_POINT('Ctrl Pts',(5.18447979493221,-3.76674505660276,
5.0515625));
#310113=CARTESIAN_POINT('Ctrl Pts',(5.7964246247213,-1.88337252830138,5.1390625));
#310114=CARTESIAN_POINT('Ctrl Pts',(5.88101256057792,-1.62303763067182,
5.15115745370687));
#310115=CARTESIAN_POINT('Ctrl Pts',(5.94192215234639,-1.3561680006146,5.16355600592057));
#310116=CARTESIAN_POINT('Ctrl Pts',(-4.95790425747066,-1.04777297948999E-14,
3.25790425747067));
#310117=CARTESIAN_POINT('Ctrl Pts',(-4.97293934348226,-0.415247004317136,
3.27293934348227));
#310118=CARTESIAN_POINT('Ctrl Pts',(-4.93570645798768,-0.831585854766426,
3.28787516811917));
#310119=CARTESIAN_POINT('Ctrl Pts',(-4.81116404609656,-1.40037558121051,
3.30810675581896));
#310120=CARTESIAN_POINT('Ctrl Pts',(-4.76783934596157,-1.55936796833944,
3.3136842461998));
#310121=CARTESIAN_POINT('Ctrl Pts',(-4.51360017410534,-2.3411247830559,
3.34192695424601));
#310122=CARTESIAN_POINT('Ctrl Pts',(-4.1901531859331,-2.92122112343498,
3.36542530920946));
#310123=CARTESIAN_POINT('Ctrl Pts',(-3.2864586721934,-3.98792201363658,
3.41441993821744));
#310124=CARTESIAN_POINT('Ctrl Pts',(-2.72857552162265,-4.3959419628284,
3.43666822694452));
#310125=CARTESIAN_POINT('Ctrl Pts',(-1.87695867632202,-4.82850004309927,
3.4696467797169));
#310126=CARTESIAN_POINT('Ctrl Pts',(-1.56418953111277,-4.95087589862769,
3.48128567849256));
#310127=CARTESIAN_POINT('Ctrl Pts',(-0.523733741453605,-5.24549600297378,
3.51854708885451));
#310128=CARTESIAN_POINT('Ctrl Pts',(0.176903345415829,-5.27616946074267,
3.54074355018794));
#310129=CARTESIAN_POINT('Ctrl Pts',(1.47610604773998,-5.11882248397312,
3.5847936147163));
#310130=CARTESIAN_POINT('Ctrl Pts',(2.12250830516505,-4.91118018333939,
3.60777680635765));
#310131=CARTESIAN_POINT('Ctrl Pts',(3.0241129566501,-4.41733830816663,3.64154899360656));
#310132=CARTESIAN_POINT('Ctrl Pts',(3.31754320793393,-4.21542459697997,
3.65273593097732));
#310133=CARTESIAN_POINT('Ctrl Pts',(4.11730640597835,-3.54210984184061,
3.68693489746714));
#310134=CARTESIAN_POINT('Ctrl Pts',(4.55655622643784,-2.99790903685779,
3.7101723791838));
#310135=CARTESIAN_POINT('Ctrl Pts',(5.23423769051958,-1.71858963227232,
3.75726483203539));
#310136=CARTESIAN_POINT('Ctrl Pts',(5.42487105484502,-1.02156461381141,
3.77925028508346));
#310137=CARTESIAN_POINT('Ctrl Pts',(5.52448070077831,0.00449183181578057,
3.81280309470563));
#310138=CARTESIAN_POINT('Ctrl Pts',(5.52414060342832,0.36457952165459,3.82450282693855));
#310139=CARTESIAN_POINT('Ctrl Pts',(5.41076537903406,1.50994706424661,3.86148648007847));
#310140=CARTESIAN_POINT('Ctrl Pts',(5.16954783102153,2.21447136914349,3.88356695868298));
#310141=CARTESIAN_POINT('Ctrl Pts',(4.50111020165292,3.45957691336163,3.92856148806867));
#310142=CARTESIAN_POINT('Ctrl Pts',(4.02525674415986,4.03647908758549,3.95223762409383));
#310143=CARTESIAN_POINT('Ctrl Pts',(3.30978474626372,4.61990466858687,3.98022046020723));
#310144=CARTESIAN_POINT('Ctrl Pts',(3.16227443582965,4.72868251477364,3.98570890981966));
#310145=CARTESIAN_POINT('Ctrl Pts',(2.39909092990884,5.23751197929896,4.01377576741889));
#310146=CARTESIAN_POINT('Ctrl Pts',(1.7146646306617,5.5238562776682,4.03699780574988));
#310147=CARTESIAN_POINT('Ctrl Pts',(0.194599395436199,5.83902880107215,
4.08488183438802));
#310148=CARTESIAN_POINT('Ctrl Pts',(-0.578175813405361,5.8207566644236,
4.10694279906758));
#310149=CARTESIAN_POINT('Ctrl Pts',(-2.02680681744372,5.54378769497724,
4.15214335059165));
#310150=CARTESIAN_POINT('Ctrl Pts',(-2.74802952750779,5.25050360603337,
4.17583159622874));
#310151=CARTESIAN_POINT('Ctrl Pts',(-3.6315318414213,4.6671975741733,4.20661545875264));
#310152=CARTESIAN_POINT('Ctrl Pts',(-3.86096261856221,4.49047984541216,
4.21504771190775));
#310153=CARTESIAN_POINT('Ctrl Pts',(-4.39279983820927,4.01526358263747,
4.23628931942137));
#310154=CARTESIAN_POINT('Ctrl Pts',(-4.6778048743089,3.69990131114164,4.24908677333639));
#310155=CARTESIAN_POINT('Ctrl Pts',(-5.17919548705663,3.00960849983932,
4.27475272437034));
#310156=CARTESIAN_POINT('Ctrl Pts',(-5.39318105256691,2.63599175969816,
4.28754473902495));
#310157=CARTESIAN_POINT('Ctrl Pts',(-5.56513300460777,2.24260889167615,
4.29999999999997));
#310158=CARTESIAN_POINT('Ctrl Pts',(6.,-1.04083408558608E-14,3.53125));
#310159=CARTESIAN_POINT('Ctrl Pts',(6.,-0.662567985849171,3.49998165563862));
#310160=CARTESIAN_POINT('Ctrl Pts',(5.89023888002911,-1.32148209989238,
3.46918647000026));
#310161=CARTESIAN_POINT('Ctrl Pts',(5.42118520370331,-2.68662270594139,
3.40405471308885));
#310162=CARTESIAN_POINT('Ctrl Pts',(5.02683829399696,-3.36719274876381,
3.36713193121169));
#310163=CARTESIAN_POINT('Ctrl Pts',(4.00167806548415,-4.53760947497116,
3.29400874410852));
#310164=CARTESIAN_POINT('Ctrl Pts',(3.38128471508339,-5.01699639073162,
3.25984728204102));
#310165=CARTESIAN_POINT('Ctrl Pts',(1.97963641525498,-5.71895831696652,
3.18670031794793));
#310166=CARTESIAN_POINT('Ctrl Pts',(1.20940416388651,-5.92982580166838,
3.14905492163172));
#310167=CARTESIAN_POINT('Ctrl Pts',(-0.351704872679288,-6.03949474463185,
3.07738850564888));
#310168=CARTESIAN_POINT('Ctrl Pts',(-1.12714151140623,-5.94380189291677,
3.04234108152995));
#310169=CARTESIAN_POINT('Ctrl Pts',(-2.60896859694703,-5.45977628556974,
2.96877370020871));
#310170=CARTESIAN_POINT('Ctrl Pts',(-3.29994699398712,-5.07210022951635,
2.93336335474523));
#310171=CARTESIAN_POINT('Ctrl Pts',(-4.49288000432945,-4.05324074403939,
2.86137269782642));
#310172=CARTESIAN_POINT('Ctrl Pts',(-4.98351548479417,-3.43209332791639,
2.82404768881904));
#310173=CARTESIAN_POINT('Ctrl Pts',(-5.69345137673978,-2.04535878292572,
2.75140961508628));
#310174=CARTESIAN_POINT('Ctrl Pts',(-5.90952163651921,-1.29476718768151,
2.71735350508463));
#310175=CARTESIAN_POINT('Ctrl Pts',(-6.04658161225873,0.26905624612609,
2.64355252059243));
#310176=CARTESIAN_POINT('Ctrl Pts',(-5.95760903598733,1.06796514813261,
2.60584988600272));
#310177=CARTESIAN_POINT('Ctrl Pts',(-5.47869485417073,2.56676990467233,
2.53511730571077));
#310178=CARTESIAN_POINT('Ctrl Pts',(-5.10034667160623,3.25439864082902,
2.49847743196067));
#310179=CARTESIAN_POINT('Ctrl Pts',(-4.10177951121022,4.44760592024899,
2.4252217782941));
#310180=CARTESIAN_POINT('Ctrl Pts',(-3.49086707735637,4.9416249658674,2.39086482120847));
#310181=CARTESIAN_POINT('Ctrl Pts',(-2.10493394767083,5.67379433086644,
2.31798267413971));
#310182=CARTESIAN_POINT('Ctrl Pts',(-1.34128866378715,5.90115742150157,
2.28039235900721));
#310183=CARTESIAN_POINT('Ctrl Pts',(0.214674357637074,6.04584984343904,
2.20844615196138));
#310184=CARTESIAN_POINT('Ctrl Pts',(0.991534561947968,5.96785131509141,
2.17377823337649));
#310185=CARTESIAN_POINT('Ctrl Pts',(2.48618119626386,5.51716889269461,2.10012172850341));
#310186=CARTESIAN_POINT('Ctrl Pts',(3.18810038614419,5.14355910318655,2.06419416006495));
#310187=CARTESIAN_POINT('Ctrl Pts',(4.40347232140798,4.1498821543838,1.99254252722497));
#310188=CARTESIAN_POINT('Ctrl Pts',(4.90648185944318,3.54096946358727,1.95534139008017));
#310189=CARTESIAN_POINT('Ctrl Pts',(5.64672397480825,2.17128984430686,1.88251379882356));
#310190=CARTESIAN_POINT('Ctrl Pts',(5.87958059376345,1.42496250709134,1.84849776826742));
#310191=CARTESIAN_POINT('Ctrl Pts',(5.98807536338565,0.437063488405821,
1.80187618773491));
#310192=CARTESIAN_POINT('Ctrl Pts',(6.,0.218403025168987,1.7915570192741));
#310193=CARTESIAN_POINT('Ctrl Pts',(6.,1.45716771982052E-14,1.78125));
#310194=CARTESIAN_POINT('Ctrl Pts',(-5.92794875776504,-0.927050983124583,
-4.30000000000003));
#310195=CARTESIAN_POINT('Ctrl Pts',(-5.77238411891593,-1.50027234926652,
-4.23487103723538));
#310196=CARTESIAN_POINT('Ctrl Pts',(-5.49784136204396,-2.18887483338659,
-4.15810865263192));
#310197=CARTESIAN_POINT('Ctrl Pts',(-4.59274666464774,-3.41508210903204,
-3.9830747098422));
#310198=CARTESIAN_POINT('Ctrl Pts',(-4.09211140668953,-3.8857077507361,
-3.90229607039226));
#310199=CARTESIAN_POINT('Ctrl Pts',(-3.37691945330692,-4.34821209201474,
-3.80291028591777));
#310200=CARTESIAN_POINT('Ctrl Pts',(-3.22602442370764,-4.43666223235013,
-3.7828527767864));
#310201=CARTESIAN_POINT('Ctrl Pts',(-2.49281137727437,-4.81852268766255,
-3.68617149588514));
#310202=CARTESIAN_POINT('Ctrl Pts',(-1.86226786933467,-5.00930313816897,
-3.60488089526184));
#310203=CARTESIAN_POINT('Ctrl Pts',(-0.978780411324384,-5.10442789867345,
-3.49216045408453));
#310204=CARTESIAN_POINT('Ctrl Pts',(-0.74299602777313,-5.11379701624593,
-3.46219799972188));
#310205=CARTESIAN_POINT('Ctrl Pts',(-0.187938582543416,-5.09834966075881,
-3.39195548336746));
#310206=CARTESIAN_POINT('Ctrl Pts',(0.167559191316829,-5.05999760683309,
-3.34821426240374));
#310207=CARTESIAN_POINT('Ctrl Pts',(0.86973501763252,-4.8885779974458,-3.25416402103133));
#310208=CARTESIAN_POINT('Ctrl Pts',(1.18664663868521,-4.77514585561402,
-3.20913740493096));
#310209=CARTESIAN_POINT('Ctrl Pts',(1.48910022457092,-4.629759453695,-3.16334165753295));
#310210=CARTESIAN_POINT('Origin',(9.215,5.3202827305824,5.));
#310211=CARTESIAN_POINT('',(9.5,5.3202827305819,4.19845583392694));
#310212=CARTESIAN_POINT('',(9.3575,5.56709997066096,4.19845583392679));
#310213=CARTESIAN_POINT('Ctrl Pts',(9.5,5.3202827305819,4.19845583392693));
#310214=CARTESIAN_POINT('Ctrl Pts',(9.50000000000002,5.33130549100061,4.19534623936907));
#310215=CARTESIAN_POINT('Ctrl Pts',(9.49935753322888,5.34243846979206,4.19252178224802));
#310216=CARTESIAN_POINT('Ctrl Pts',(9.49353446737686,5.39198941174876,4.18140331781018));
#310217=CARTESIAN_POINT('Ctrl Pts',(9.48064078915421,5.43017938720461,4.17694939724907));
#310218=CARTESIAN_POINT('Ctrl Pts',(9.44299369100292,5.49538607396019,4.17694939724907));
#310219=CARTESIAN_POINT('Ctrl Pts',(9.41636704119957,5.52564731457715,4.18140331781018));
#310220=CARTESIAN_POINT('Ctrl Pts',(9.37636619960977,5.55546570851116,4.19252178224798));
#310221=CARTESIAN_POINT('Ctrl Pts',(9.36704599054229,5.56158859045169,4.19534623936898));
#310222=CARTESIAN_POINT('Ctrl Pts',(9.3575,5.56709997066096,4.19845583392679));
#310223=CARTESIAN_POINT('',(9.5,5.32028273058909,-4.19845583392491));
#310224=CARTESIAN_POINT('',(9.5,5.3202827305824,5.));
#310225=CARTESIAN_POINT('',(9.35750000000016,5.56709997066087,-4.19845583392674));
#310226=CARTESIAN_POINT('Ctrl Pts',(9.35750000000016,5.56709997066087,-4.19845583392674));
#310227=CARTESIAN_POINT('Ctrl Pts',(9.3670459905424,5.56158859045162,-4.19534623936895));
#310228=CARTESIAN_POINT('Ctrl Pts',(9.37636619960982,5.55546570851112,-4.19252178224797));
#310229=CARTESIAN_POINT('Ctrl Pts',(9.41636704119957,5.52564731457715,-4.18140331781018));
#310230=CARTESIAN_POINT('Ctrl Pts',(9.44299369100292,5.49538607396019,-4.17694939724907));
#310231=CARTESIAN_POINT('Ctrl Pts',(9.48064078915421,5.43017938720461,-4.17694939724907));
#310232=CARTESIAN_POINT('Ctrl Pts',(9.49353446737686,5.39198941174876,-4.18140331781018));
#310233=CARTESIAN_POINT('Ctrl Pts',(9.4993575332286,5.34243846979447,-4.19252178224748));
#310234=CARTESIAN_POINT('Ctrl Pts',(9.49999999999974,5.33130549100545,-4.19534623936784));
#310235=CARTESIAN_POINT('Ctrl Pts',(9.5,5.32028273058909,-4.1984558339249));
#310236=CARTESIAN_POINT('',(9.3575,5.56709997066097,5.));
#310237=CARTESIAN_POINT('Origin',(-2.11419423634674E-15,10.6405654611648,
5.));
#310238=CARTESIAN_POINT('',(0.142500000000837,10.8873827012429,4.19845583392707));
#310239=CARTESIAN_POINT('',(-0.142499999999995,10.8873827012434,4.19845583392679));
#310240=CARTESIAN_POINT('Ctrl Pts',(0.142500000000829,10.8873827012429,
4.19845583392706));
#310241=CARTESIAN_POINT('Ctrl Pts',(0.132954009458285,10.8928940814523,
4.19534623936915));
#310242=CARTESIAN_POINT('Ctrl Pts',(0.122991333619391,10.8979041783033,
4.19252178224805));
#310243=CARTESIAN_POINT('Ctrl Pts',(0.0771674261772861,10.9176367263259,
4.18140331781018));
#310244=CARTESIAN_POINT('Ctrl Pts',(0.0376470981512924,10.9255654611648,
4.17694939724907));
#310245=CARTESIAN_POINT('Ctrl Pts',(-0.0376470981512968,10.9255654611648,
4.17694939724907));
#310246=CARTESIAN_POINT('Ctrl Pts',(-0.0771674261772924,10.9176367263259,
4.18140331781018));
#310247=CARTESIAN_POINT('Ctrl Pts',(-0.122991333619098,10.8979041783034,
4.19252178224798));
#310248=CARTESIAN_POINT('Ctrl Pts',(-0.13295400945771,10.8928940814526,
4.19534623936898));
#310249=CARTESIAN_POINT('Ctrl Pts',(-0.142499999999999,10.8873827012434,
4.19845583392679));
#310250=CARTESIAN_POINT('',(0.142499999990597,10.8873827012488,-4.19845583392373));
#310251=CARTESIAN_POINT('',(0.142499999999998,10.8873827012434,5.));
#310252=CARTESIAN_POINT('',(-0.142499999999839,10.8873827012435,-4.19845583392674));
#310253=CARTESIAN_POINT('Ctrl Pts',(-0.142499999999839,10.8873827012435,
-4.19845583392674));
#310254=CARTESIAN_POINT('Ctrl Pts',(-0.132954009457597,10.8928940814527,
-4.19534623936895));
#310255=CARTESIAN_POINT('Ctrl Pts',(-0.122991333619039,10.8979041783034,
-4.19252178224797));
#310256=CARTESIAN_POINT('Ctrl Pts',(-0.0771674261772909,10.9176367263259,
-4.18140331781018));
#310257=CARTESIAN_POINT('Ctrl Pts',(-0.0376470981512967,10.9255654611648,
-4.17694939724907));
#310258=CARTESIAN_POINT('Ctrl Pts',(0.0376470981512925,10.9255654611648,
-4.17694939724907));
#310259=CARTESIAN_POINT('Ctrl Pts',(0.0771674261772871,10.9176367263259,
-4.18140331781018));
#310260=CARTESIAN_POINT('Ctrl Pts',(0.122991333615721,10.8979041783048,
-4.19252178224716));
#310261=CARTESIAN_POINT('Ctrl Pts',(0.132954009451165,10.8928940814559,
-4.19534623936713));
#310262=CARTESIAN_POINT('Ctrl Pts',(0.142499999990594,10.8873827012488,
-4.19845583392373));
#310263=CARTESIAN_POINT('',(-0.142500000000002,10.8873827012434,5.));
#310264=CARTESIAN_POINT('Origin',(-9.215,5.3202827305824,5.));
#310265=CARTESIAN_POINT('',(-9.35749999999916,5.56709997066145,4.19845583392707));
#310266=CARTESIAN_POINT('',(-9.5,5.32028273058247,4.19845583392678));
#310267=CARTESIAN_POINT('Ctrl Pts',(-9.35749999999916,5.56709997066145,
4.19845583392706));
#310268=CARTESIAN_POINT('Ctrl Pts',(-9.36704599054174,5.56158859045205,
4.19534623936915));
#310269=CARTESIAN_POINT('Ctrl Pts',(-9.37636619960951,5.55546570851135,
4.19252178224805));
#310270=CARTESIAN_POINT('Ctrl Pts',(-9.41636704119957,5.52564731457715,
4.18140331781018));
#310271=CARTESIAN_POINT('Ctrl Pts',(-9.44299369100292,5.49538607396019,
4.17694939724907));
#310272=CARTESIAN_POINT('Ctrl Pts',(-9.48064078915421,5.43017938720461,
4.17694939724907));
#310273=CARTESIAN_POINT('Ctrl Pts',(-9.49353446737686,5.39198941174876,
4.18140331781018));
#310274=CARTESIAN_POINT('Ctrl Pts',(-9.49935753322886,5.34243846979225,
4.19252178224798));
#310275=CARTESIAN_POINT('Ctrl Pts',(-9.5,5.33130549100099,4.19534623936897));
#310276=CARTESIAN_POINT('Ctrl Pts',(-9.5,5.32028273058247,4.19845583392677));
#310277=CARTESIAN_POINT('',(-9.3575000000094,5.56709997065554,-4.19845583392373));
#310278=CARTESIAN_POINT('',(-9.3575,5.56709997066097,5.));
#310279=CARTESIAN_POINT('',(-9.5,5.32028273058339,-4.19845583392652));
#310280=CARTESIAN_POINT('Ctrl Pts',(-9.5,5.32028273058339,-4.19845583392651));
#310281=CARTESIAN_POINT('Ctrl Pts',(-9.49999999999996,5.33130549100161,
-4.19534623936881));
#310282=CARTESIAN_POINT('Ctrl Pts',(-9.49935753322882,5.34243846979256,
-4.19252178224791));
#310283=CARTESIAN_POINT('Ctrl Pts',(-9.49353446737686,5.39198941174876,
-4.18140331781018));
#310284=CARTESIAN_POINT('Ctrl Pts',(-9.48064078915421,5.43017938720461,
-4.17694939724907));
#310285=CARTESIAN_POINT('Ctrl Pts',(-9.44299369100292,5.49538607396019,
-4.17694939724907));
#310286=CARTESIAN_POINT('Ctrl Pts',(-9.41636704119957,5.52564731457715,
-4.18140331781018));
#310287=CARTESIAN_POINT('Ctrl Pts',(-9.37636619961271,5.55546570850896,
-4.19252178224716));
#310288=CARTESIAN_POINT('Ctrl Pts',(-9.36704599054841,5.56158859044768,
-4.19534623936713));
#310289=CARTESIAN_POINT('Ctrl Pts',(-9.3575000000094,5.56709997065554,-4.19845583392373));
#310290=CARTESIAN_POINT('',(-9.5,5.3202827305824,5.));
#310291=CARTESIAN_POINT('Origin',(-9.215,-5.3202827305824,5.));
#310292=CARTESIAN_POINT('',(-9.5,-5.3202827305819,4.19845583392694));
#310293=CARTESIAN_POINT('',(-9.3575,-5.56709997066096,4.19845583392679));
#310294=CARTESIAN_POINT('Ctrl Pts',(-9.5,-5.3202827305819,4.19845583392693));
#310295=CARTESIAN_POINT('Ctrl Pts',(-9.50000000000002,-5.33130549100061,
4.19534623936907));
#310296=CARTESIAN_POINT('Ctrl Pts',(-9.49935753322888,-5.34243846979206,
4.19252178224802));
#310297=CARTESIAN_POINT('Ctrl Pts',(-9.49353446737686,-5.39198941174876,
4.18140331781018));
#310298=CARTESIAN_POINT('Ctrl Pts',(-9.48064078915421,-5.43017938720461,
4.17694939724907));
#310299=CARTESIAN_POINT('Ctrl Pts',(-9.44299369100292,-5.49538607396019,
4.17694939724907));
#310300=CARTESIAN_POINT('Ctrl Pts',(-9.41636704119957,-5.52564731457715,
4.18140331781018));
#310301=CARTESIAN_POINT('Ctrl Pts',(-9.37636619960977,-5.55546570851116,
4.19252178224798));
#310302=CARTESIAN_POINT('Ctrl Pts',(-9.36704599054229,-5.56158859045169,
4.19534623936898));
#310303=CARTESIAN_POINT('Ctrl Pts',(-9.3575,-5.56709997066096,4.19845583392679));
#310304=CARTESIAN_POINT('',(-9.5,-5.32028273058909,-4.19845583392491));
#310305=CARTESIAN_POINT('',(-9.5,-5.3202827305824,5.));
#310306=CARTESIAN_POINT('',(-9.35750000000016,-5.56709997066087,-4.19845583392674));
#310307=CARTESIAN_POINT('Ctrl Pts',(-9.35750000000016,-5.56709997066087,
-4.19845583392674));
#310308=CARTESIAN_POINT('Ctrl Pts',(-9.36704599054239,-5.56158859045162,
-4.19534623936895));
#310309=CARTESIAN_POINT('Ctrl Pts',(-9.37636619960982,-5.55546570851112,
-4.19252178224797));
#310310=CARTESIAN_POINT('Ctrl Pts',(-9.41636704119957,-5.52564731457715,
-4.18140331781018));
#310311=CARTESIAN_POINT('Ctrl Pts',(-9.44299369100292,-5.49538607396019,
-4.17694939724907));
#310312=CARTESIAN_POINT('Ctrl Pts',(-9.48064078915421,-5.43017938720461,
-4.17694939724907));
#310313=CARTESIAN_POINT('Ctrl Pts',(-9.49353446737686,-5.39198941174876,
-4.18140331781018));
#310314=CARTESIAN_POINT('Ctrl Pts',(-9.4993575332286,-5.34243846979447,
-4.19252178224748));
#310315=CARTESIAN_POINT('Ctrl Pts',(-9.49999999999974,-5.33130549100545,
-4.19534623936784));
#310316=CARTESIAN_POINT('Ctrl Pts',(-9.5,-5.32028273058909,-4.1984558339249));
#310317=CARTESIAN_POINT('',(-9.3575,-5.56709997066097,5.));
#310318=CARTESIAN_POINT('Origin',(-1.62630325872825E-15,-10.6405654611648,
5.));
#310319=CARTESIAN_POINT('',(-0.142500000000841,-10.8873827012429,4.19845583392707));
#310320=CARTESIAN_POINT('',(0.142499999999992,-10.8873827012434,4.19845583392679));
#310321=CARTESIAN_POINT('Ctrl Pts',(-0.142500000000832,-10.8873827012429,
4.19845583392706));
#310322=CARTESIAN_POINT('Ctrl Pts',(-0.132954009458289,-10.8928940814523,
4.19534623936915));
#310323=CARTESIAN_POINT('Ctrl Pts',(-0.122991333619395,-10.8979041783033,
4.19252178224806));
#310324=CARTESIAN_POINT('Ctrl Pts',(-0.0771674261772907,-10.9176367263259,
4.18140331781018));
#310325=CARTESIAN_POINT('Ctrl Pts',(-0.0376470981512962,-10.9255654611648,
4.17694939724907));
#310326=CARTESIAN_POINT('Ctrl Pts',(0.037647098151293,-10.9255654611648,
4.17694939724907));
#310327=CARTESIAN_POINT('Ctrl Pts',(0.0771674261772873,-10.9176367263259,
4.18140331781018));
#310328=CARTESIAN_POINT('Ctrl Pts',(0.122991333619093,-10.8979041783034,
4.19252178224798));
#310329=CARTESIAN_POINT('Ctrl Pts',(0.132954009457706,-10.8928940814526,
4.19534623936898));
#310330=CARTESIAN_POINT('Ctrl Pts',(0.142499999999995,-10.8873827012434,
4.19845583392679));
#310331=CARTESIAN_POINT('',(-0.1424999999906,-10.8873827012488,-4.19845583392373));
#310332=CARTESIAN_POINT('',(-0.142500000000002,-10.8873827012434,5.));
#310333=CARTESIAN_POINT('',(0.142499999999835,-10.8873827012435,-4.19845583392674));
#310334=CARTESIAN_POINT('Ctrl Pts',(0.142499999999835,-10.8873827012435,
-4.19845583392674));
#310335=CARTESIAN_POINT('Ctrl Pts',(0.132954009457593,-10.8928940814527,
-4.19534623936895));
#310336=CARTESIAN_POINT('Ctrl Pts',(0.122991333619035,-10.8979041783034,
-4.19252178224797));
#310337=CARTESIAN_POINT('Ctrl Pts',(0.0771674261772873,-10.9176367263259,
-4.18140331781018));
#310338=CARTESIAN_POINT('Ctrl Pts',(0.0376470981512929,-10.9255654611648,
-4.17694939724907));
#310339=CARTESIAN_POINT('Ctrl Pts',(-0.0376470981512963,-10.9255654611648,
-4.17694939724907));
#310340=CARTESIAN_POINT('Ctrl Pts',(-0.0771674261772907,-10.9176367263259,
-4.18140331781018));
#310341=CARTESIAN_POINT('Ctrl Pts',(-0.122991333615725,-10.8979041783048,
-4.19252178224716));
#310342=CARTESIAN_POINT('Ctrl Pts',(-0.132954009451169,-10.8928940814559,
-4.19534623936713));
#310343=CARTESIAN_POINT('Ctrl Pts',(-0.142499999990597,-10.8873827012488,
-4.19845583392373));
#310344=CARTESIAN_POINT('',(0.142499999999998,-10.8873827012434,5.));
#310345=CARTESIAN_POINT('Origin',(9.215,-5.3202827305824,5.));
#310346=CARTESIAN_POINT('',(9.35749999999916,-5.56709997066145,4.19845583392707));
#310347=CARTESIAN_POINT('',(9.5,-5.32028273058247,4.19845583392678));
#310348=CARTESIAN_POINT('Ctrl Pts',(9.35749999999916,-5.56709997066145,
4.19845583392706));
#310349=CARTESIAN_POINT('Ctrl Pts',(9.36704599054174,-5.56158859045205,
4.19534623936915));
#310350=CARTESIAN_POINT('Ctrl Pts',(9.3763661996095,-5.55546570851135,4.19252178224805));
#310351=CARTESIAN_POINT('Ctrl Pts',(9.41636704119957,-5.52564731457715,
4.18140331781018));
#310352=CARTESIAN_POINT('Ctrl Pts',(9.44299369100292,-5.49538607396019,
4.17694939724907));
#310353=CARTESIAN_POINT('Ctrl Pts',(9.48064078915421,-5.43017938720461,
4.17694939724907));
#310354=CARTESIAN_POINT('Ctrl Pts',(9.49353446737686,-5.39198941174876,
4.18140331781018));
#310355=CARTESIAN_POINT('Ctrl Pts',(9.49935753322886,-5.34243846979225,
4.19252178224798));
#310356=CARTESIAN_POINT('Ctrl Pts',(9.5,-5.33130549100099,4.19534623936897));
#310357=CARTESIAN_POINT('Ctrl Pts',(9.5,-5.32028273058247,4.19845583392677));
#310358=CARTESIAN_POINT('',(9.3575000000094,-5.56709997065554,-4.19845583392373));
#310359=CARTESIAN_POINT('',(9.3575,-5.56709997066097,5.));
#310360=CARTESIAN_POINT('',(9.5,-5.3202827305834,-4.19845583392651));
#310361=CARTESIAN_POINT('Ctrl Pts',(9.5,-5.3202827305834,-4.19845583392651));
#310362=CARTESIAN_POINT('Ctrl Pts',(9.49999999999996,-5.33130549100162,
-4.19534623936881));
#310363=CARTESIAN_POINT('Ctrl Pts',(9.49935753322882,-5.34243846979256,
-4.19252178224791));
#310364=CARTESIAN_POINT('Ctrl Pts',(9.49353446737686,-5.39198941174876,
-4.18140331781018));
#310365=CARTESIAN_POINT('Ctrl Pts',(9.48064078915421,-5.43017938720461,
-4.17694939724907));
#310366=CARTESIAN_POINT('Ctrl Pts',(9.44299369100292,-5.49538607396019,
-4.17694939724907));
#310367=CARTESIAN_POINT('Ctrl Pts',(9.41636704119957,-5.52564731457715,
-4.18140331781018));
#310368=CARTESIAN_POINT('Ctrl Pts',(9.37636619961271,-5.55546570850896,
-4.19252178224716));
#310369=CARTESIAN_POINT('Ctrl Pts',(9.36704599054841,-5.56158859044768,
-4.19534623936713));
#310370=CARTESIAN_POINT('Ctrl Pts',(9.3575000000094,-5.56709997065554,-4.19845583392373));
#310371=CARTESIAN_POINT('',(9.5,-5.3202827305824,5.));
#310372=CARTESIAN_POINT('Origin',(0.,0.,-5.));
#310373=CARTESIAN_POINT('',(9.5,0.,-5.));
#310374=CARTESIAN_POINT('Ctrl Pts',(9.5,-5.32028273061113,-4.19845583391869));
#310375=CARTESIAN_POINT('Ctrl Pts',(9.5,-2.47900257549584,-5.));
#310376=CARTESIAN_POINT('Ctrl Pts',(9.5,-8.86951651586679E-16,-5.));
#310377=CARTESIAN_POINT('',(4.75,-8.22724133595217,-5.));
#310378=CARTESIAN_POINT('Ctrl Pts',(4.75000000000002,-8.22724133595217,
-4.99999999999999));
#310379=CARTESIAN_POINT('Ctrl Pts',(6.89687920642992,-6.98774004820225,
-4.99999999999999));
#310380=CARTESIAN_POINT('Ctrl Pts',(9.3575000000334,-5.56709997064169,-4.1984558339159));
#310381=CARTESIAN_POINT('Origin',(0.,0.,-5.));
#310382=CARTESIAN_POINT('Origin',(0.,0.,-5.));
#310383=CARTESIAN_POINT('Ctrl Pts',(0.142499999975816,-10.8873827012573,
-4.1984558339189));
#310384=CARTESIAN_POINT('Ctrl Pts',(2.60312079357385,-9.46674262369993,
-5.));
#310385=CARTESIAN_POINT('Ctrl Pts',(4.75000000000002,-8.22724133595217,
-4.99999999999999));
#310386=CARTESIAN_POINT('',(-4.75,-8.22724133595217,-5.));
#310387=CARTESIAN_POINT('Ctrl Pts',(-4.74999999999998,-8.22724133595218,
-5.));
#310388=CARTESIAN_POINT('Ctrl Pts',(-2.60312079357007,-9.4667426237021,
-5.));
#310389=CARTESIAN_POINT('Ctrl Pts',(-0.142499999966577,-10.8873827012627,
-4.1984558339159));
#310390=CARTESIAN_POINT('Origin',(0.,0.,-5.));
#310391=CARTESIAN_POINT('Origin',(0.,0.,-5.));
#310392=CARTESIAN_POINT('Ctrl Pts',(-9.35750000002419,-5.567099970647,-4.19845583391891));
#310393=CARTESIAN_POINT('Ctrl Pts',(-6.89687920642616,-6.98774004820442,
-5.));
#310394=CARTESIAN_POINT('Ctrl Pts',(-4.74999999999998,-8.22724133595218,
-5.));
#310395=CARTESIAN_POINT('',(-9.5,0.,-5.));
#310396=CARTESIAN_POINT('Ctrl Pts',(-9.5,8.86951651586679E-16,-5.));
#310397=CARTESIAN_POINT('Ctrl Pts',(-9.5,-2.47900257549816,-5.));
#310398=CARTESIAN_POINT('Ctrl Pts',(-9.5,-5.32028273061684,-4.19845583391707));
#310399=CARTESIAN_POINT('Origin',(0.,0.,-5.));
#310400=CARTESIAN_POINT('Origin',(0.,0.,-5.));
#310401=CARTESIAN_POINT('Ctrl Pts',(-9.5,5.32028273061112,-4.19845583391869));
#310402=CARTESIAN_POINT('Ctrl Pts',(-9.5,2.47900257549584,-5.));
#310403=CARTESIAN_POINT('Ctrl Pts',(-9.5,8.86951651586679E-16,-5.));
#310404=CARTESIAN_POINT('',(-4.75,8.22724133595217,-5.));
#310405=CARTESIAN_POINT('Ctrl Pts',(-4.75,8.22724133595217,-5.));
#310406=CARTESIAN_POINT('Ctrl Pts',(-6.89687920642992,6.98774004820225,
-5.));
#310407=CARTESIAN_POINT('Ctrl Pts',(-9.35750000003342,5.56709997064168,
-4.1984558339159));
#310408=CARTESIAN_POINT('Origin',(0.,0.,-5.));
#310409=CARTESIAN_POINT('Origin',(0.,0.,-5.));
#310410=CARTESIAN_POINT('Ctrl Pts',(-0.142499999975832,10.8873827012573,
-4.19845583391891));
#310411=CARTESIAN_POINT('Ctrl Pts',(-2.60312079357384,9.46674262369993,
-5.));
#310412=CARTESIAN_POINT('Ctrl Pts',(-4.75,8.22724133595217,-5.));
#310413=CARTESIAN_POINT('',(4.75,8.22724133595217,-5.));
#310414=CARTESIAN_POINT('Ctrl Pts',(4.74999999999998,8.22724133595218,-5.));
#310415=CARTESIAN_POINT('Ctrl Pts',(2.60312079357007,9.46674262370209,-5.));
#310416=CARTESIAN_POINT('Ctrl Pts',(0.142499999966585,10.8873827012627,
-4.1984558339159));
#310417=CARTESIAN_POINT('Origin',(0.,0.,-5.));
#310418=CARTESIAN_POINT('Origin',(0.,0.,-5.));
#310419=CARTESIAN_POINT('Ctrl Pts',(9.35750000002419,5.567099970647,-4.19845583391891));
#310420=CARTESIAN_POINT('Ctrl Pts',(6.89687920642616,6.98774004820442,-5.));
#310421=CARTESIAN_POINT('Ctrl Pts',(4.74999999999998,8.22724133595218,-5.));
#310422=CARTESIAN_POINT('Ctrl Pts',(9.5,-8.86951651586679E-16,-5.));
#310423=CARTESIAN_POINT('Ctrl Pts',(9.5,2.47900257549816,-5.));
#310424=CARTESIAN_POINT('Ctrl Pts',(9.5,5.32028273061684,-4.19845583391707));
#310425=CARTESIAN_POINT('Origin',(0.,0.,-5.));
#310426=CARTESIAN_POINT('Origin',(0.,0.,5.));
#310427=CARTESIAN_POINT('',(4.75,8.22724133595217,5.));
#310428=CARTESIAN_POINT('Ctrl Pts',(4.75,8.22724133595218,4.99999999999999));
#310429=CARTESIAN_POINT('Ctrl Pts',(2.60312079357424,9.46674262369969,4.99999999999999));
#310430=CARTESIAN_POINT('Ctrl Pts',(0.142499999976817,10.8873827012568,
4.19845583391923));
#310431=CARTESIAN_POINT('',(-4.75,8.22724133595217,5.));
#310432=CARTESIAN_POINT('Ctrl Pts',(-0.14249999997599,10.8873827012572,
4.19845583391897));
#310433=CARTESIAN_POINT('Ctrl Pts',(-2.60312079357392,9.46674262369989,
5.));
#310434=CARTESIAN_POINT('Ctrl Pts',(-4.75000000000002,8.22724133595217,
5.));
#310435=CARTESIAN_POINT('Origin',(0.,0.,5.));
#310436=CARTESIAN_POINT('Origin',(0.,0.,5.));
#310437=CARTESIAN_POINT('Ctrl Pts',(-4.75000000000002,8.22724133595217,
5.));
#310438=CARTESIAN_POINT('Ctrl Pts',(-6.89687920642577,6.98774004820465,
4.99999999999999));
#310439=CARTESIAN_POINT('Ctrl Pts',(-9.35750000002319,5.56709997064759,
4.19845583391923));
#310440=CARTESIAN_POINT('',(-9.5,0.,5.));
#310441=CARTESIAN_POINT('Ctrl Pts',(-9.5,5.32028273061021,4.19845583391894));
#310442=CARTESIAN_POINT('Ctrl Pts',(-9.5,2.47900257549547,5.));
#310443=CARTESIAN_POINT('Ctrl Pts',(-9.5,-8.86951651586679E-16,5.));
#310444=CARTESIAN_POINT('Origin',(0.,0.,5.));
#310445=CARTESIAN_POINT('Origin',(0.,0.,5.));
#310446=CARTESIAN_POINT('Ctrl Pts',(-9.5,-8.86951651586679E-16,5.));
#310447=CARTESIAN_POINT('Ctrl Pts',(-9.5,-2.47900257549523,5.));
#310448=CARTESIAN_POINT('Ctrl Pts',(-9.5,-5.32028273060964,4.19845583391911));
#310449=CARTESIAN_POINT('',(-4.75,-8.22724133595217,5.));
#310450=CARTESIAN_POINT('Ctrl Pts',(-9.35750000002403,-5.5670999706471,
4.19845583391896));
#310451=CARTESIAN_POINT('Ctrl Pts',(-6.8968792064261,-6.98774004820445,
5.));
#310452=CARTESIAN_POINT('Ctrl Pts',(-4.75,-8.22724133595218,4.99999999999999));
#310453=CARTESIAN_POINT('Origin',(0.,0.,5.));
#310454=CARTESIAN_POINT('Origin',(0.,0.,5.));
#310455=CARTESIAN_POINT('Ctrl Pts',(-4.75,-8.22724133595218,4.99999999999999));
#310456=CARTESIAN_POINT('Ctrl Pts',(-2.60312079357424,-9.46674262369969,
4.99999999999999));
#310457=CARTESIAN_POINT('Ctrl Pts',(-0.142499999976817,-10.8873827012568,
4.19845583391923));
#310458=CARTESIAN_POINT('',(4.75,-8.22724133595217,5.));
#310459=CARTESIAN_POINT('Ctrl Pts',(0.142499999975978,-10.8873827012572,
4.19845583391896));
#310460=CARTESIAN_POINT('Ctrl Pts',(2.6031207935739,-9.46674262369989,4.99999999999999));
#310461=CARTESIAN_POINT('Ctrl Pts',(4.75,-8.22724133595218,4.99999999999999));
#310462=CARTESIAN_POINT('Origin',(0.,0.,5.));
#310463=CARTESIAN_POINT('Origin',(0.,0.,5.));
#310464=CARTESIAN_POINT('Ctrl Pts',(4.75,-8.22724133595218,4.99999999999999));
#310465=CARTESIAN_POINT('Ctrl Pts',(6.89687920642576,-6.98774004820466,
5.));
#310466=CARTESIAN_POINT('Ctrl Pts',(9.35750000002319,-5.56709997064759,
4.19845583391923));
#310467=CARTESIAN_POINT('',(9.5,0.,5.));
#310468=CARTESIAN_POINT('Ctrl Pts',(9.5,-5.32028273061021,4.19845583391894));
#310469=CARTESIAN_POINT('Ctrl Pts',(9.5,-2.47900257549547,5.));
#310470=CARTESIAN_POINT('Ctrl Pts',(9.5,8.86951651586679E-16,5.));
#310471=CARTESIAN_POINT('Origin',(0.,0.,5.));
#310472=CARTESIAN_POINT('Origin',(0.,0.,5.));
#310473=CARTESIAN_POINT('Ctrl Pts',(9.5,8.86951651586679E-16,5.));
#310474=CARTESIAN_POINT('Ctrl Pts',(9.5,2.47900257549523,5.));
#310475=CARTESIAN_POINT('Ctrl Pts',(9.5,5.32028273060964,4.19845583391911));
#310476=CARTESIAN_POINT('Ctrl Pts',(9.35750000002403,5.5670999706471,4.19845583391896));
#310477=CARTESIAN_POINT('Ctrl Pts',(6.8968792064261,6.98774004820445,5.));
#310478=CARTESIAN_POINT('Ctrl Pts',(4.75,8.22724133595218,4.99999999999999));
#310479=CARTESIAN_POINT('Origin',(0.,0.,5.));
#310480=CARTESIAN_POINT('Origin',(0.,8.67361737988403E-16,5.));
#310481=CARTESIAN_POINT('Origin',(9.5,-5.48482755730145,5.));
#310482=CARTESIAN_POINT('Origin',(-1.04722137768024E-15,-10.9696551146029,
5.));
#310483=CARTESIAN_POINT('Origin',(-9.5,-5.48482755730145,5.));
#310484=CARTESIAN_POINT('Origin',(-9.5,5.48482755730145,5.));
#310485=CARTESIAN_POINT('Origin',(-1.87852400592822E-15,10.9696551146029,
5.));
#310486=CARTESIAN_POINT('Origin',(9.5,5.48482755730145,5.));
#310487=CARTESIAN_POINT('Origin',(0.,0.,5.));
#310488=CARTESIAN_POINT('',(-6.7,4.68483825596759E-17,5.));
#310489=CARTESIAN_POINT('Origin',(0.,8.67361737988403E-16,5.));
#310490=CARTESIAN_POINT('Origin',(0.,0.,-5.));
#310491=CARTESIAN_POINT('',(6.7,4.68483825596763E-17,-5.));
#310492=CARTESIAN_POINT('Origin',(0.,8.67361737988403E-16,-5.));
#310493=CARTESIAN_POINT('Origin',(0.,8.67361737988403E-16,-5.));
#310494=CARTESIAN_POINT('',(6.7,4.68483825596764E-17,-5.));
#310495=CARTESIAN_POINT('Origin',(0.,8.67361737988403E-16,4.3));
#310496=CARTESIAN_POINT('',(-6.,1.32573658499991E-16,4.3));
#310600=UNCERTAINTY_MEASURE_WITH_UNIT(LENGTH_MEASURE(0.01),#310624,
'DISTANCE_ACCURACY_VALUE',
'Maximum model space distance between geometric entities at asserted c
onnectivities');
#310601=UNCERTAINTY_MEASURE_WITH_UNIT(LENGTH_MEASURE(0.01),#310624,
'DISTANCE_ACCURACY_VALUE',
'Maximum model space distance between geometric entities at asserted c
onnectivities');
#310622=(
GEOMETRIC_REPRESENTATION_CONTEXT(3)
GLOBAL_UNCERTAINTY_ASSIGNED_CONTEXT((#310600))
GLOBAL_UNIT_ASSIGNED_CONTEXT((#310624,#310626,#310627))
REPRESENTATION_CONTEXT('','3D')
);
#310623=(
GEOMETRIC_REPRESENTATION_CONTEXT(3)
GLOBAL_UNCERTAINTY_ASSIGNED_CONTEXT((#310601))
GLOBAL_UNIT_ASSIGNED_CONTEXT((#310624,#310626,#310627))
REPRESENTATION_CONTEXT('','3D')
);
#310624=(
LENGTH_UNIT()
NAMED_UNIT(*)
SI_UNIT(.MILLI.,.METRE.)
);
#310626=(
NAMED_UNIT(*)
PLANE_ANGLE_UNIT()
SI_UNIT($,.RADIAN.)
);
#310627=(
NAMED_UNIT(*)
SI_UNIT($,.STERADIAN.)
SOLID_ANGLE_UNIT()
);
#310648=SHAPE_DEFINITION_REPRESENTATION(#310809,#310913);
#310809=PRODUCT_DEFINITION_SHAPE('',$,#310935);
#310913=SHAPE_REPRESENTATION('',(#104720),#310622);
#310914=PRODUCT_DEFINITION_CONTEXT('part definition',#310979,'design');
#310935=PRODUCT_DEFINITION('Zinc-Plated Steel Hex Nut',
'Zinc-Plated Steel Hex Nut',#310956,#310914);
#310956=PRODUCT_DEFINITION_FORMATION('',$,#311001);
#310979=APPLICATION_CONTEXT(
'Core Data for Automotive Mechanical Design Process');
#310980=PRODUCT_CONTEXT('part definition',#310979,'mechanical');
#311001=PRODUCT('Zinc-Plated Steel Hex Nut','Zinc-Plated Steel Hex Nut',
$,(#310980));
#311008=PRESENTATION_STYLE_ASSIGNMENT((#311015));
#311015=SURFACE_STYLE_USAGE(.BOTH.,#311022);
#311022=SURFACE_SIDE_STYLE('',(#311029));
#311029=SURFACE_STYLE_FILL_AREA(#311036);
#311036=FILL_AREA_STYLE('Opaque(31,36,43)',(#311043));
#311043=FILL_AREA_STYLE_COLOUR('Opaque(31,36,43)',#311050);
#311050=COLOUR_RGB('Opaque(31,36,43)',0.12156862745098,0.141176470588235,
0.168627450980392);
ENDSEC;
END-ISO-10303-21;
